ISO-10303-21;
HEADER;
/* Generated by software containing ST-Developer
 * from STEP Tools, Inc. (www.steptools.com) 
 */

FILE_DESCRIPTION(
/* description */ ('Ball-race swivel caster'),
/* implementation_level */ '2;1');

FILE_NAME(
/* name */ 'Housing washer.step',
/* time_stamp */ '2026-10-29T16:15:51-07:00',
/* author */ (''),
/* organization */ (''),
/* preprocessor_version */ 'ST-DEVELOPER v20.2',
/* originating_system */ 'Autodesk Translation Framework v15.17.0.0',
/* authorisation */ '');

FILE_SCHEMA (('AUTOMOTIVE_DESIGN { 1 0 10303 214 3 1 1 }'));
ENDSEC;

DATA;
#10=MECHANICAL_DESIGN_GEOMETRIC_PRESENTATION_REPRESENTATION('',(#301),#7816);
#180=TOROIDAL_SURFACE('',#4146,1.1,0.208);
#181=TOROIDAL_SURFACE('',#4148,1.1,0.208);
#182=TOROIDAL_SURFACE('',#4150,1.1,0.208);
#183=TOROIDAL_SURFACE('',#4152,1.1,0.208);
#184=TOROIDAL_SURFACE('',#4154,1.1,0.208);
#185=TOROIDAL_SURFACE('',#4156,1.1,0.208);
#186=TOROIDAL_SURFACE('',#4158,1.1,0.208);
#187=TOROIDAL_SURFACE('',#4160,1.1,0.208);
#188=TOROIDAL_SURFACE('',#4162,1.1,0.208);
#189=TOROIDAL_SURFACE('',#4164,1.1,0.208);
#218=B_SPLINE_CURVE_WITH_KNOTS('',3,(#6296,#6297,#6298,#6299,#6300,#6301,
#6302,#6303,#6304,#6305,#6306,#6307,#6308,#6309,#6310,#6311),
 .UNSPECIFIED.,.F.,.F.,(4,2,2,2,2,2,2,4),(-0.464072133285216,-0.409463462974853,
-0.354653577959658,-0.295254131517975,-0.239649525442001,-0.179869516594444,
-0.105654793183195,0.),.UNSPECIFIED.);
#219=B_SPLINE_CURVE_WITH_KNOTS('',3,(#6315,#6316,#6317,#6318,#6319,#6320,
#6321,#6322),.UNSPECIFIED.,.F.,.F.,(4,2,2,4),(-0.178087805736112,-0.164911408034075,
-0.098411128398998,0.),.UNSPECIFIED.);
#220=B_SPLINE_CURVE_WITH_KNOTS('',3,(#6327,#6328,#6329,#6330,#6331,#6332,
#6333,#6334,#6335,#6336,#6337,#6338),.UNSPECIFIED.,.F.,.F.,(4,2,2,2,2,4),
(-0.454179041892585,-0.395759356749908,-0.338728191012637,-0.275894647345938,
-0.221135020913471,-0.178087805736112),.UNSPECIFIED.);
#221=B_SPLINE_CURVE_WITH_KNOTS('',3,(#6343,#6344,#6345,#6346,#6347,#6348,
#6349,#6350,#6351,#6352,#6353,#6354,#6355,#6356,#6357,#6358),
 .UNSPECIFIED.,.F.,.F.,(4,2,2,2,2,2,2,4),(-0.464097123055979,-0.409448749757929,
-0.354953921831334,-0.295351891164134,-0.23977302109073,-0.179990573569022,
-0.105700836781514,0.),.UNSPECIFIED.);
#222=B_SPLINE_CURVE_WITH_KNOTS('',3,(#6362,#6363,#6364,#6365,#6366,#6367,
#6368,#6369,#6370,#6371,#6372,#6373,#6374,#6375,#6376,#6377),
 .UNSPECIFIED.,.F.,.F.,(4,2,2,2,2,2,2,4),(-0.454248309090339,-0.396054469342525,
-0.339406675181652,-0.276261577769397,-0.221379042231507,-0.16516447777942,
-0.0986090884438264,0.),.UNSPECIFIED.);
#223=B_SPLINE_CURVE_WITH_KNOTS('',3,(#6387,#6388,#6389,#6390,#6391,#6392,
#6393,#6394,#6395,#6396,#6397,#6398,#6399,#6400,#6401,#6402),
 .UNSPECIFIED.,.F.,.F.,(4,2,2,2,2,2,2,4),(-0.464064837962443,-0.40946685218913,
-0.354565796864779,-0.295225270188433,-0.239612954364833,-0.179833767169879,
-0.10564139145842,0.),.UNSPECIFIED.);
#224=B_SPLINE_CURVE_WITH_KNOTS('',3,(#6411,#6412,#6413,#6414,#6415,#6416,
#6417,#6418,#6419,#6420,#6421,#6422,#6423,#6424,#6425,#6426),
 .UNSPECIFIED.,.F.,.F.,(4,2,2,2,2,2,2,4),(-0.454158667319305,-0.395672852804848,
-0.338529950359406,-0.275786564377698,-0.221062756831303,-0.164836364834586,
-0.0983527839094943,0.),.UNSPECIFIED.);
#225=B_SPLINE_CURVE_WITH_KNOTS('',3,(#6431,#6432,#6433,#6434,#6435,#6436,
#6437,#6438,#6439,#6440,#6441,#6442,#6443,#6444),.UNSPECIFIED.,.F.,.F.,
(4,2,2,2,2,2,4),(-0.46407213328519,-0.409463462974826,-0.35465357795963,
-0.295254131517947,-0.239649525441978,-0.179869516594429,-0.153354495923151),
 .UNSPECIFIED.);
#226=B_SPLINE_CURVE_WITH_KNOTS('',3,(#6448,#6449,#6450,#6451,#6452,#6453,
#6454,#6455,#6456,#6457,#6458,#6459,#6460,#6461,#6462,#6463),
 .UNSPECIFIED.,.F.,.F.,(4,2,2,2,2,2,2,4),(-0.45417904189259,-0.395759356749915,
-0.338728191012647,-0.275894647345947,-0.221135020913479,-0.164911408034082,
-0.0984111283990018,0.),.UNSPECIFIED.);
#227=B_SPLINE_CURVE_WITH_KNOTS('',3,(#6466,#6467,#6468,#6469,#6470,#6471),
 .UNSPECIFIED.,.F.,.F.,(4,2,4),(-0.153354495923151,-0.105654793183189,0.),
 .UNSPECIFIED.);
#228=B_SPLINE_CURVE_WITH_KNOTS('',3,(#6478,#6479,#6480,#6481),
 .UNSPECIFIED.,.F.,.F.,(4,4),(-0.464097123055929,-0.436632642152621),
 .UNSPECIFIED.);
#229=B_SPLINE_CURVE_WITH_KNOTS('',3,(#6485,#6486,#6487,#6488,#6489,#6490,
#6491,#6492,#6493,#6494,#6495,#6496,#6497,#6498,#6499,#6500),
 .UNSPECIFIED.,.F.,.F.,(4,2,2,2,2,2,2,4),(-0.454248309090296,-0.396054469342484,
-0.339406675181621,-0.276261577769375,-0.221379042231491,-0.165164477779409,
-0.0986090884438205,0.),.UNSPECIFIED.);
#230=B_SPLINE_CURVE_WITH_KNOTS('',3,(#6503,#6504,#6505,#6506,#6507,#6508,
#6509,#6510,#6511,#6512,#6513,#6514,#6515,#6516,#6517,#6518),
 .UNSPECIFIED.,.F.,.F.,(4,2,2,2,2,2,2,4),(-0.436632642152621,-0.409448749757886,
-0.354953921831299,-0.295351891164106,-0.239773021090707,-0.179990573569004,
-0.105700836781506,0.),.UNSPECIFIED.);
#231=B_SPLINE_CURVE_WITH_KNOTS('',3,(#6525,#6526,#6527,#6528,#6529,#6530,
#6531,#6532,#6533,#6534),.UNSPECIFIED.,.F.,.F.,(4,2,2,2,4),(-0.46407213328521,
-0.40946346297485,-0.354653577959657,-0.295254131517975,-0.285596349669175),
 .UNSPECIFIED.);
#232=B_SPLINE_CURVE_WITH_KNOTS('',3,(#6538,#6539,#6540,#6541,#6542,#6543,
#6544,#6545,#6546,#6547,#6548,#6549,#6550,#6551,#6552,#6553),
 .UNSPECIFIED.,.F.,.F.,(4,2,2,2,2,2,2,4),(-0.454179041892491,-0.395759356749834,
-0.338728191012574,-0.275894647345886,-0.221135020913429,-0.164911408034045,
-0.0984111283989847,0.),.UNSPECIFIED.);
#233=B_SPLINE_CURVE_WITH_KNOTS('',3,(#6556,#6557,#6558,#6559,#6560,#6561,
#6562,#6563,#6564,#6565),.UNSPECIFIED.,.F.,.F.,(4,2,2,2,4),(-0.285596349669175,
-0.239649525442001,-0.179869516594444,-0.105654793183195,0.),
 .UNSPECIFIED.);
#234=B_SPLINE_CURVE_WITH_KNOTS('',3,(#6572,#6573,#6574,#6575,#6576,#6577,
#6578,#6579,#6580,#6581,#6582,#6583,#6584,#6585,#6586,#6587),
 .UNSPECIFIED.,.F.,.F.,(4,2,2,2,2,2,2,4),(-0.464097123056155,-0.409448749758082,
-0.354953921831466,-0.295351891164244,-0.239773021090817,-0.179990573569081,
-0.10570083678154,0.),.UNSPECIFIED.);
#235=B_SPLINE_CURVE_WITH_KNOTS('',3,(#6591,#6592,#6593,#6594,#6595,#6596,
#6597,#6598,#6599,#6600,#6601,#6602,#6603,#6604,#6605,#6606),
 .UNSPECIFIED.,.F.,.F.,(4,2,2,2,2,2,2,4),(-0.454248309090326,-0.396054469342517,
-0.339406675181648,-0.276261577769394,-0.221379042231504,-0.165164477779418,
-0.0986090884438254,0.),.UNSPECIFIED.);
#236=B_SPLINE_CURVE_WITH_KNOTS('',3,(#6616,#6617,#6618,#6619,#6620,#6621,
#6622,#6623,#6624,#6625,#6626,#6627,#6628,#6629,#6630,#6631),
 .UNSPECIFIED.,.F.,.F.,(4,2,2,2,2,2,2,4),(-0.464064837962487,-0.409466852189169,
-0.35456579686481,-0.295225270188456,-0.23961295436485,-0.17983376716989,
-0.105641391458424,0.),.UNSPECIFIED.);
#237=B_SPLINE_CURVE_WITH_KNOTS('',3,(#6635,#6636,#6637,#6638,#6639,#6640,
#6641,#6642,#6643,#6644,#6645,#6646,#6647,#6648,#6649,#6650),
 .UNSPECIFIED.,.F.,.F.,(4,2,2,2,2,2,2,4),(-0.454158667319304,-0.395672852804846,
-0.338529950359405,-0.275786564377698,-0.221062756831303,-0.164836364834585,
-0.0983527839094934,0.),.UNSPECIFIED.);
#238=B_SPLINE_CURVE_WITH_KNOTS('',3,(#6660,#6661,#6662,#6663,#6664,#6665,
#6666,#6667,#6668,#6669,#6670,#6671,#6672,#6673,#6674,#6675),
 .UNSPECIFIED.,.F.,.F.,(4,2,2,2,2,2,2,4),(-0.464072133285175,-0.409463462974818,
-0.354653577959626,-0.295254131517947,-0.23964952544198,-0.179869516594429,
-0.105654793183188,0.),.UNSPECIFIED.);
#239=B_SPLINE_CURVE_WITH_KNOTS('',3,(#6679,#6680,#6681,#6682,#6683,#6684,
#6685,#6686,#6687,#6688,#6689,#6690),.UNSPECIFIED.,.F.,.F.,(4,2,2,2,2,4),
(-0.307335875219043,-0.275894647345908,-0.221135020913448,-0.164911408034059,
-0.0984111283989903,0.),.UNSPECIFIED.);
#240=B_SPLINE_CURVE_WITH_KNOTS('',3,(#6695,#6696,#6697,#6698,#6699,#6700,
#6701,#6702),.UNSPECIFIED.,.F.,.F.,(4,2,2,4),(-0.454179041892519,-0.395759356749857,
-0.338728191012597,-0.307335875219043),.UNSPECIFIED.);
#241=B_SPLINE_CURVE_WITH_KNOTS('',3,(#6707,#6708,#6709,#6710,#6711,#6712,
#6713,#6714,#6715,#6716,#6717,#6718,#6719,#6720,#6721,#6722),
 .UNSPECIFIED.,.F.,.F.,(4,2,2,2,2,2,2,4),(-0.464097123055928,-0.409448749757884,
-0.354953921831297,-0.295351891164106,-0.239773021090708,-0.179990573569004,
-0.105700836781506,0.),.UNSPECIFIED.);
#242=B_SPLINE_CURVE_WITH_KNOTS('',3,(#6726,#6727,#6728,#6729),
 .UNSPECIFIED.,.F.,.F.,(4,4),(-0.028880024024466,0.),.UNSPECIFIED.);
#243=B_SPLINE_CURVE_WITH_KNOTS('',3,(#6734,#6735,#6736,#6737,#6738,#6739,
#6740,#6741,#6742,#6743,#6744,#6745,#6746,#6747,#6748,#6749),
 .UNSPECIFIED.,.F.,.F.,(4,2,2,2,2,2,2,4),(-0.454248309090515,-0.396054469342676,
-0.339406675181783,-0.276261577769502,-0.221379042231587,-0.165164477779474,
-0.0986090884438518,-0.028880024024466),.UNSPECIFIED.);
#261=SHAPE_REPRESENTATION_RELATIONSHIP('SRR','None',#7907,#281);
#281=ADVANCED_BREP_SHAPE_REPRESENTATION('',(#337),#7796);
#301=STYLED_ITEM('',(#8104),#337);
#337=MANIFOLD_SOLID_BREP('Body1',#3707);
#395=FACE_BOUND('',#815,.T.);
#396=FACE_BOUND('',#827,.T.);
#397=FACE_BOUND('',#828,.T.);
#398=FACE_BOUND('',#829,.T.);
#399=FACE_BOUND('',#830,.T.);
#400=FACE_BOUND('',#831,.T.);
#401=FACE_BOUND('',#832,.T.);
#402=FACE_BOUND('',#833,.T.);
#403=FACE_BOUND('',#834,.T.);
#404=FACE_BOUND('',#835,.T.);
#405=FACE_BOUND('',#836,.T.);
#406=FACE_BOUND('',#837,.T.);
#407=FACE_BOUND('',#840,.T.);
#452=PLANE('',#4134);
#453=PLANE('',#4166);
#454=PLANE('',#4171);
#569=FACE_OUTER_BOUND('',#804,.T.);
#570=FACE_OUTER_BOUND('',#805,.T.);
#571=FACE_OUTER_BOUND('',#806,.T.);
#572=FACE_OUTER_BOUND('',#807,.T.);
#573=FACE_OUTER_BOUND('',#808,.T.);
#574=FACE_OUTER_BOUND('',#809,.T.);
#575=FACE_OUTER_BOUND('',#810,.T.);
#576=FACE_OUTER_BOUND('',#811,.T.);
#577=FACE_OUTER_BOUND('',#812,.T.);
#578=FACE_OUTER_BOUND('',#813,.T.);
#579=FACE_OUTER_BOUND('',#814,.T.);
#580=FACE_OUTER_BOUND('',#816,.T.);
#581=FACE_OUTER_BOUND('',#817,.T.);
#582=FACE_OUTER_BOUND('',#818,.T.);
#583=FACE_OUTER_BOUND('',#819,.T.);
#584=FACE_OUTER_BOUND('',#820,.T.);
#585=FACE_OUTER_BOUND('',#821,.T.);
#586=FACE_OUTER_BOUND('',#822,.T.);
#587=FACE_OUTER_BOUND('',#823,.T.);
#588=FACE_OUTER_BOUND('',#824,.T.);
#589=FACE_OUTER_BOUND('',#825,.T.);
#590=FACE_OUTER_BOUND('',#826,.T.);
#591=FACE_OUTER_BOUND('',#838,.T.);
#592=FACE_OUTER_BOUND('',#839,.T.);
#593=FACE_OUTER_BOUND('',#841,.T.);
#804=EDGE_LOOP('',(#2703,#2704,#2705,#2706,#2707,#2708,#2709,#2710));
#805=EDGE_LOOP('',(#2711,#2712,#2713,#2714,#2715,#2716,#2717,#2718));
#806=EDGE_LOOP('',(#2719,#2720,#2721,#2722,#2723,#2724,#2725,#2726));
#807=EDGE_LOOP('',(#2727,#2728,#2729,#2730,#2731,#2732,#2733,#2734));
#808=EDGE_LOOP('',(#2735,#2736,#2737,#2738,#2739,#2740,#2741,#2742));
#809=EDGE_LOOP('',(#2743,#2744,#2745,#2746,#2747,#2748,#2749,#2750));
#810=EDGE_LOOP('',(#2751,#2752,#2753,#2754,#2755,#2756,#2757,#2758));
#811=EDGE_LOOP('',(#2759,#2760,#2761,#2762,#2763,#2764,#2765,#2766));
#812=EDGE_LOOP('',(#2767,#2768,#2769,#2770,#2771,#2772,#2773,#2774));
#813=EDGE_LOOP('',(#2775,#2776,#2777,#2778,#2779,#2780,#2781,#2782));
#814=EDGE_LOOP('',(#2783,#2784,#2785,#2786,#2787,#2788,#2789,#2790,#2791,
#2792,#2793,#2794,#2795,#2796,#2797,#2798,#2799,#2800,#2801,#2802,#2803));
#815=EDGE_LOOP('',(#2804));
#816=EDGE_LOOP('',(#2805,#2806,#2807,#2808));
#817=EDGE_LOOP('',(#2809,#2810,#2811,#2812,#2813));
#818=EDGE_LOOP('',(#2814,#2815,#2816,#2817,#2818));
#819=EDGE_LOOP('',(#2819,#2820,#2821,#2822,#2823));
#820=EDGE_LOOP('',(#2824,#2825,#2826,#2827));
#821=EDGE_LOOP('',(#2828,#2829,#2830,#2831));
#822=EDGE_LOOP('',(#2832,#2833,#2834,#2835,#2836));
#823=EDGE_LOOP('',(#2837,#2838,#2839,#2840));
#824=EDGE_LOOP('',(#2841,#2842,#2843,#2844,#2845));
#825=EDGE_LOOP('',(#2846,#2847,#2848,#2849,#2850));
#826=EDGE_LOOP('',(#2851));
#827=EDGE_LOOP('',(#2852));
#828=EDGE_LOOP('',(#2853));
#829=EDGE_LOOP('',(#2854));
#830=EDGE_LOOP('',(#2855));
#831=EDGE_LOOP('',(#2856));
#832=EDGE_LOOP('',(#2857));
#833=EDGE_LOOP('',(#2858));
#834=EDGE_LOOP('',(#2859));
#835=EDGE_LOOP('',(#2860));
#836=EDGE_LOOP('',(#2861));
#837=EDGE_LOOP('',(#2862));
#838=EDGE_LOOP('',(#2863,#2864,#2865,#2866));
#839=EDGE_LOOP('',(#2867));
#840=EDGE_LOOP('',(#2868,#2869,#2870,#2871,#2872,#2873,#2874,#2875,#2876,
#2877,#2878,#2879,#2880,#2881,#2882,#2883,#2884,#2885,#2886,#2887,#2888,
#2889,#2890));
#841=EDGE_LOOP('',(#2891,#2892,#2893,#2894));
#1044=LINE('',#6324,#1199);
#1045=LINE('',#6381,#1200);
#1046=LINE('',#6406,#1201);
#1047=LINE('',#6473,#1202);
#1048=LINE('',#6520,#1203);
#1049=LINE('',#6567,#1204);
#1050=LINE('',#6610,#1205);
#1051=LINE('',#6654,#1206);
#1052=LINE('',#6692,#1207);
#1053=LINE('',#6731,#1208);
#1054=LINE('',#6792,#1209);
#1055=LINE('',#6795,#1210);
#1199=VECTOR('',#4782,0.22);
#1200=VECTOR('',#4793,0.22);
#1201=VECTOR('',#4802,0.22);
#1202=VECTOR('',#4815,0.22);
#1203=VECTOR('',#4824,0.22);
#1204=VECTOR('',#4833,0.22);
#1205=VECTOR('',#4842,0.22);
#1206=VECTOR('',#4853,0.22);
#1207=VECTOR('',#4862,0.22);
#1208=VECTOR('',#4871,0.22);
#1209=VECTOR('',#4950,1.4);
#1210=VECTOR('',#4955,0.8);
#1397=CIRCLE('',#4091,0.22);
#1398=CIRCLE('',#4092,0.22);
#1399=CIRCLE('',#4093,0.22);
#1400=CIRCLE('',#4095,0.22);
#1401=CIRCLE('',#4096,0.22);
#1402=CIRCLE('',#4097,0.22);
#1403=CIRCLE('',#4098,0.22);
#1404=CIRCLE('',#4100,0.22);
#1405=CIRCLE('',#4101,0.22);
#1406=CIRCLE('',#4102,0.22);
#1407=CIRCLE('',#4103,0.22);
#1408=CIRCLE('',#4105,0.22);
#1409=CIRCLE('',#4106,0.22);
#1410=CIRCLE('',#4107,0.22);
#1411=CIRCLE('',#4109,0.22);
#1412=CIRCLE('',#4110,0.22);
#1413=CIRCLE('',#4111,0.22);
#1414=CIRCLE('',#4113,0.22);
#1415=CIRCLE('',#4114,0.22);
#1416=CIRCLE('',#4115,0.22);
#1417=CIRCLE('',#4117,0.22);
#1418=CIRCLE('',#4118,0.22);
#1419=CIRCLE('',#4119,0.22);
#1420=CIRCLE('',#4120,0.22);
#1421=CIRCLE('',#4122,0.22);
#1422=CIRCLE('',#4123,0.22);
#1423=CIRCLE('',#4124,0.22);
#1424=CIRCLE('',#4125,0.22);
#1425=CIRCLE('',#4127,0.22);
#1426=CIRCLE('',#4128,0.22);
#1427=CIRCLE('',#4129,0.22);
#1428=CIRCLE('',#4131,0.22);
#1429=CIRCLE('',#4132,0.22);
#1430=CIRCLE('',#4133,0.22);
#1431=CIRCLE('',#4135,0.917615790157152);
#1432=CIRCLE('',#4136,0.917615790157152);
#1433=CIRCLE('',#4137,0.917615790157152);
#1434=CIRCLE('',#4138,0.917615790157152);
#1435=CIRCLE('',#4139,0.917615790157152);
#1436=CIRCLE('',#4140,0.917615790157152);
#1437=CIRCLE('',#4141,0.917615790157152);
#1438=CIRCLE('',#4142,0.917615790157152);
#1439=CIRCLE('',#4143,0.917615790157152);
#1440=CIRCLE('',#4144,0.917615790157152);
#1441=CIRCLE('',#4145,0.8);
#1442=CIRCLE('',#4147,1.28238420984285);
#1443=CIRCLE('',#4149,1.28238420984285);
#1444=CIRCLE('',#4151,1.28238420984285);
#1445=CIRCLE('',#4153,1.28238420984285);
#1446=CIRCLE('',#4155,1.28238420984285);
#1447=CIRCLE('',#4157,1.28238420984285);
#1448=CIRCLE('',#4159,1.28238420984285);
#1449=CIRCLE('',#4161,1.28238420984285);
#1450=CIRCLE('',#4163,1.28238420984285);
#1451=CIRCLE('',#4165,1.28238420984285);
#1452=CIRCLE('',#4167,1.4);
#1453=CIRCLE('',#4168,0.8);
#1454=CIRCLE('',#4170,1.4);
#1675=VERTEX_POINT('',#6294);
#1676=VERTEX_POINT('',#6295);
#1677=VERTEX_POINT('',#6312);
#1678=VERTEX_POINT('',#6314);
#1679=VERTEX_POINT('',#6323);
#1680=VERTEX_POINT('',#6326);
#1681=VERTEX_POINT('',#6341);
#1682=VERTEX_POINT('',#6342);
#1683=VERTEX_POINT('',#6359);
#1684=VERTEX_POINT('',#6361);
#1685=VERTEX_POINT('',#6378);
#1686=VERTEX_POINT('',#6380);
#1687=VERTEX_POINT('',#6385);
#1688=VERTEX_POINT('',#6386);
#1689=VERTEX_POINT('',#6403);
#1690=VERTEX_POINT('',#6405);
#1691=VERTEX_POINT('',#6408);
#1692=VERTEX_POINT('',#6410);
#1693=VERTEX_POINT('',#6429);
#1694=VERTEX_POINT('',#6430);
#1695=VERTEX_POINT('',#6445);
#1696=VERTEX_POINT('',#6447);
#1697=VERTEX_POINT('',#6464);
#1698=VERTEX_POINT('',#6472);
#1699=VERTEX_POINT('',#6476);
#1700=VERTEX_POINT('',#6477);
#1701=VERTEX_POINT('',#6482);
#1702=VERTEX_POINT('',#6484);
#1703=VERTEX_POINT('',#6501);
#1704=VERTEX_POINT('',#6519);
#1705=VERTEX_POINT('',#6523);
#1706=VERTEX_POINT('',#6524);
#1707=VERTEX_POINT('',#6535);
#1708=VERTEX_POINT('',#6537);
#1709=VERTEX_POINT('',#6554);
#1710=VERTEX_POINT('',#6566);
#1711=VERTEX_POINT('',#6570);
#1712=VERTEX_POINT('',#6571);
#1713=VERTEX_POINT('',#6588);
#1714=VERTEX_POINT('',#6590);
#1715=VERTEX_POINT('',#6607);
#1716=VERTEX_POINT('',#6609);
#1717=VERTEX_POINT('',#6614);
#1718=VERTEX_POINT('',#6615);
#1719=VERTEX_POINT('',#6632);
#1720=VERTEX_POINT('',#6634);
#1721=VERTEX_POINT('',#6651);
#1722=VERTEX_POINT('',#6653);
#1723=VERTEX_POINT('',#6658);
#1724=VERTEX_POINT('',#6659);
#1725=VERTEX_POINT('',#6676);
#1726=VERTEX_POINT('',#6678);
#1727=VERTEX_POINT('',#6691);
#1728=VERTEX_POINT('',#6694);
#1729=VERTEX_POINT('',#6705);
#1730=VERTEX_POINT('',#6706);
#1731=VERTEX_POINT('',#6723);
#1732=VERTEX_POINT('',#6725);
#1733=VERTEX_POINT('',#6730);
#1734=VERTEX_POINT('',#6733);
#1735=VERTEX_POINT('',#6762);
#1736=VERTEX_POINT('',#6785);
#1737=VERTEX_POINT('',#6787);
#1738=VERTEX_POINT('',#6790);
#2071=EDGE_CURVE('',#1675,#1676,#218,.T.);
#2072=EDGE_CURVE('',#1677,#1675,#1397,.T.);
#2073=EDGE_CURVE('',#1678,#1677,#219,.T.);
#2074=EDGE_CURVE('',#1678,#1679,#1044,.T.);
#2075=EDGE_CURVE('',#1679,#1679,#1398,.T.);
#2076=EDGE_CURVE('',#1680,#1678,#220,.T.);
#2077=EDGE_CURVE('',#1676,#1680,#1399,.T.);
#2078=EDGE_CURVE('',#1681,#1682,#221,.T.);
#2079=EDGE_CURVE('',#1683,#1681,#1400,.T.);
#2080=EDGE_CURVE('',#1684,#1683,#222,.T.);
#2081=EDGE_CURVE('',#1685,#1684,#1401,.T.);
#2082=EDGE_CURVE('',#1685,#1686,#1045,.T.);
#2083=EDGE_CURVE('',#1686,#1686,#1402,.T.);
#2084=EDGE_CURVE('',#1682,#1685,#1403,.T.);
#2085=EDGE_CURVE('',#1687,#1688,#223,.T.);
#2086=EDGE_CURVE('',#1689,#1687,#1404,.T.);
#2087=EDGE_CURVE('',#1689,#1690,#1046,.T.);
#2088=EDGE_CURVE('',#1690,#1690,#1405,.T.);
#2089=EDGE_CURVE('',#1691,#1689,#1406,.T.);
#2090=EDGE_CURVE('',#1692,#1691,#224,.T.);
#2091=EDGE_CURVE('',#1688,#1692,#1407,.T.);
#2092=EDGE_CURVE('',#1693,#1694,#225,.T.);
#2093=EDGE_CURVE('',#1695,#1693,#1408,.T.);
#2094=EDGE_CURVE('',#1696,#1695,#226,.T.);
#2095=EDGE_CURVE('',#1697,#1696,#1409,.T.);
#2096=EDGE_CURVE('',#1694,#1697,#227,.T.);
#2097=EDGE_CURVE('',#1694,#1698,#1047,.T.);
#2098=EDGE_CURVE('',#1698,#1698,#1410,.T.);
#2099=EDGE_CURVE('',#1699,#1700,#228,.T.);
#2100=EDGE_CURVE('',#1701,#1699,#1411,.T.);
#2101=EDGE_CURVE('',#1702,#1701,#229,.T.);
#2102=EDGE_CURVE('',#1703,#1702,#1412,.T.);
#2103=EDGE_CURVE('',#1700,#1703,#230,.T.);
#2104=EDGE_CURVE('',#1700,#1704,#1048,.T.);
#2105=EDGE_CURVE('',#1704,#1704,#1413,.T.);
#2106=EDGE_CURVE('',#1705,#1706,#231,.T.);
#2107=EDGE_CURVE('',#1707,#1705,#1414,.T.);
#2108=EDGE_CURVE('',#1708,#1707,#232,.T.);
#2109=EDGE_CURVE('',#1709,#1708,#1415,.T.);
#2110=EDGE_CURVE('',#1706,#1709,#233,.T.);
#2111=EDGE_CURVE('',#1706,#1710,#1049,.T.);
#2112=EDGE_CURVE('',#1710,#1710,#1416,.T.);
#2113=EDGE_CURVE('',#1711,#1712,#234,.T.);
#2114=EDGE_CURVE('',#1713,#1711,#1417,.T.);
#2115=EDGE_CURVE('',#1714,#1713,#235,.T.);
#2116=EDGE_CURVE('',#1715,#1714,#1418,.T.);
#2117=EDGE_CURVE('',#1715,#1716,#1050,.T.);
#2118=EDGE_CURVE('',#1716,#1716,#1419,.T.);
#2119=EDGE_CURVE('',#1712,#1715,#1420,.T.);
#2120=EDGE_CURVE('',#1717,#1718,#236,.T.);
#2121=EDGE_CURVE('',#1719,#1717,#1421,.T.);
#2122=EDGE_CURVE('',#1720,#1719,#237,.T.);
#2123=EDGE_CURVE('',#1721,#1720,#1422,.T.);
#2124=EDGE_CURVE('',#1721,#1722,#1051,.T.);
#2125=EDGE_CURVE('',#1722,#1722,#1423,.T.);
#2126=EDGE_CURVE('',#1718,#1721,#1424,.T.);
#2127=EDGE_CURVE('',#1723,#1724,#238,.T.);
#2128=EDGE_CURVE('',#1725,#1723,#1425,.T.);
#2129=EDGE_CURVE('',#1726,#1725,#239,.T.);
#2130=EDGE_CURVE('',#1726,#1727,#1052,.T.);
#2131=EDGE_CURVE('',#1727,#1727,#1426,.T.);
#2132=EDGE_CURVE('',#1728,#1726,#240,.T.);
#2133=EDGE_CURVE('',#1724,#1728,#1427,.T.);
#2134=EDGE_CURVE('',#1729,#1730,#241,.T.);
#2135=EDGE_CURVE('',#1731,#1729,#1428,.T.);
#2136=EDGE_CURVE('',#1732,#1731,#242,.T.);
#2137=EDGE_CURVE('',#1732,#1733,#1053,.T.);
#2138=EDGE_CURVE('',#1733,#1733,#1429,.T.);
#2139=EDGE_CURVE('',#1734,#1732,#243,.T.);
#2140=EDGE_CURVE('',#1730,#1734,#1430,.T.);
#2141=EDGE_CURVE('',#1675,#1731,#1431,.T.);
#2142=EDGE_CURVE('',#1729,#1691,#1432,.T.);
#2143=EDGE_CURVE('',#1687,#1701,#1433,.T.);
#2144=EDGE_CURVE('',#1699,#1707,#1434,.T.);
#2145=EDGE_CURVE('',#1705,#1695,#1435,.T.);
#2146=EDGE_CURVE('',#1693,#1713,#1436,.T.);
#2147=EDGE_CURVE('',#1711,#1719,#1437,.T.);
#2148=EDGE_CURVE('',#1717,#1683,#1438,.T.);
#2149=EDGE_CURVE('',#1681,#1725,#1439,.T.);
#2150=EDGE_CURVE('',#1723,#1677,#1440,.T.);
#2151=EDGE_CURVE('',#1735,#1735,#1441,.T.);
#2152=EDGE_CURVE('',#1720,#1712,#1442,.T.);
#2153=EDGE_CURVE('',#1708,#1703,#1443,.T.);
#2154=EDGE_CURVE('',#1714,#1697,#1444,.T.);
#2155=EDGE_CURVE('',#1696,#1709,#1445,.T.);
#2156=EDGE_CURVE('',#1702,#1688,#1446,.T.);
#2157=EDGE_CURVE('',#1692,#1730,#1447,.T.);
#2158=EDGE_CURVE('',#1728,#1682,#1448,.T.);
#2159=EDGE_CURVE('',#1684,#1718,#1449,.T.);
#2160=EDGE_CURVE('',#1734,#1676,#1450,.T.);
#2161=EDGE_CURVE('',#1680,#1724,#1451,.T.);
#2162=EDGE_CURVE('',#1736,#1736,#1452,.T.);
#2163=EDGE_CURVE('',#1737,#1737,#1453,.T.);
#2164=EDGE_CURVE('',#1738,#1738,#1454,.T.);
#2165=EDGE_CURVE('',#1738,#1736,#1054,.T.);
#2166=EDGE_CURVE('',#1735,#1737,#1055,.T.);
#2703=ORIENTED_EDGE('',*,*,#2071,.F.);
#2704=ORIENTED_EDGE('',*,*,#2072,.F.);
#2705=ORIENTED_EDGE('',*,*,#2073,.F.);
#2706=ORIENTED_EDGE('',*,*,#2074,.T.);
#2707=ORIENTED_EDGE('',*,*,#2075,.F.);
#2708=ORIENTED_EDGE('',*,*,#2074,.F.);
#2709=ORIENTED_EDGE('',*,*,#2076,.F.);
#2710=ORIENTED_EDGE('',*,*,#2077,.F.);
#2711=ORIENTED_EDGE('',*,*,#2078,.F.);
#2712=ORIENTED_EDGE('',*,*,#2079,.F.);
#2713=ORIENTED_EDGE('',*,*,#2080,.F.);
#2714=ORIENTED_EDGE('',*,*,#2081,.F.);
#2715=ORIENTED_EDGE('',*,*,#2082,.T.);
#2716=ORIENTED_EDGE('',*,*,#2083,.F.);
#2717=ORIENTED_EDGE('',*,*,#2082,.F.);
#2718=ORIENTED_EDGE('',*,*,#2084,.F.);
#2719=ORIENTED_EDGE('',*,*,#2085,.F.);
#2720=ORIENTED_EDGE('',*,*,#2086,.F.);
#2721=ORIENTED_EDGE('',*,*,#2087,.T.);
#2722=ORIENTED_EDGE('',*,*,#2088,.F.);
#2723=ORIENTED_EDGE('',*,*,#2087,.F.);
#2724=ORIENTED_EDGE('',*,*,#2089,.F.);
#2725=ORIENTED_EDGE('',*,*,#2090,.F.);
#2726=ORIENTED_EDGE('',*,*,#2091,.F.);
#2727=ORIENTED_EDGE('',*,*,#2092,.F.);
#2728=ORIENTED_EDGE('',*,*,#2093,.F.);
#2729=ORIENTED_EDGE('',*,*,#2094,.F.);
#2730=ORIENTED_EDGE('',*,*,#2095,.F.);
#2731=ORIENTED_EDGE('',*,*,#2096,.F.);
#2732=ORIENTED_EDGE('',*,*,#2097,.T.);
#2733=ORIENTED_EDGE('',*,*,#2098,.F.);
#2734=ORIENTED_EDGE('',*,*,#2097,.F.);
#2735=ORIENTED_EDGE('',*,*,#2099,.F.);
#2736=ORIENTED_EDGE('',*,*,#2100,.F.);
#2737=ORIENTED_EDGE('',*,*,#2101,.F.);
#2738=ORIENTED_EDGE('',*,*,#2102,.F.);
#2739=ORIENTED_EDGE('',*,*,#2103,.F.);
#2740=ORIENTED_EDGE('',*,*,#2104,.T.);
#2741=ORIENTED_EDGE('',*,*,#2105,.F.);
#2742=ORIENTED_EDGE('',*,*,#2104,.F.);
#2743=ORIENTED_EDGE('',*,*,#2106,.F.);
#2744=ORIENTED_EDGE('',*,*,#2107,.F.);
#2745=ORIENTED_EDGE('',*,*,#2108,.F.);
#2746=ORIENTED_EDGE('',*,*,#2109,.F.);
#2747=ORIENTED_EDGE('',*,*,#2110,.F.);
#2748=ORIENTED_EDGE('',*,*,#2111,.T.);
#2749=ORIENTED_EDGE('',*,*,#2112,.F.);
#2750=ORIENTED_EDGE('',*,*,#2111,.F.);
#2751=ORIENTED_EDGE('',*,*,#2113,.F.);
#2752=ORIENTED_EDGE('',*,*,#2114,.F.);
#2753=ORIENTED_EDGE('',*,*,#2115,.F.);
#2754=ORIENTED_EDGE('',*,*,#2116,.F.);
#2755=ORIENTED_EDGE('',*,*,#2117,.T.);
#2756=ORIENTED_EDGE('',*,*,#2118,.F.);
#2757=ORIENTED_EDGE('',*,*,#2117,.F.);
#2758=ORIENTED_EDGE('',*,*,#2119,.F.);
#2759=ORIENTED_EDGE('',*,*,#2120,.F.);
#2760=ORIENTED_EDGE('',*,*,#2121,.F.);
#2761=ORIENTED_EDGE('',*,*,#2122,.F.);
#2762=ORIENTED_EDGE('',*,*,#2123,.F.);
#2763=ORIENTED_EDGE('',*,*,#2124,.T.);
#2764=ORIENTED_EDGE('',*,*,#2125,.F.);
#2765=ORIENTED_EDGE('',*,*,#2124,.F.);
#2766=ORIENTED_EDGE('',*,*,#2126,.F.);
#2767=ORIENTED_EDGE('',*,*,#2127,.F.);
#2768=ORIENTED_EDGE('',*,*,#2128,.F.);
#2769=ORIENTED_EDGE('',*,*,#2129,.F.);
#2770=ORIENTED_EDGE('',*,*,#2130,.T.);
#2771=ORIENTED_EDGE('',*,*,#2131,.F.);
#2772=ORIENTED_EDGE('',*,*,#2130,.F.);
#2773=ORIENTED_EDGE('',*,*,#2132,.F.);
#2774=ORIENTED_EDGE('',*,*,#2133,.F.);
#2775=ORIENTED_EDGE('',*,*,#2134,.F.);
#2776=ORIENTED_EDGE('',*,*,#2135,.F.);
#2777=ORIENTED_EDGE('',*,*,#2136,.F.);
#2778=ORIENTED_EDGE('',*,*,#2137,.T.);
#2779=ORIENTED_EDGE('',*,*,#2138,.F.);
#2780=ORIENTED_EDGE('',*,*,#2137,.F.);
#2781=ORIENTED_EDGE('',*,*,#2139,.F.);
#2782=ORIENTED_EDGE('',*,*,#2140,.F.);
#2783=ORIENTED_EDGE('',*,*,#2072,.T.);
#2784=ORIENTED_EDGE('',*,*,#2141,.T.);
#2785=ORIENTED_EDGE('',*,*,#2135,.T.);
#2786=ORIENTED_EDGE('',*,*,#2142,.T.);
#2787=ORIENTED_EDGE('',*,*,#2089,.T.);
#2788=ORIENTED_EDGE('',*,*,#2086,.T.);
#2789=ORIENTED_EDGE('',*,*,#2143,.T.);
#2790=ORIENTED_EDGE('',*,*,#2100,.T.);
#2791=ORIENTED_EDGE('',*,*,#2144,.T.);
#2792=ORIENTED_EDGE('',*,*,#2107,.T.);
#2793=ORIENTED_EDGE('',*,*,#2145,.T.);
#2794=ORIENTED_EDGE('',*,*,#2093,.T.);
#2795=ORIENTED_EDGE('',*,*,#2146,.T.);
#2796=ORIENTED_EDGE('',*,*,#2114,.T.);
#2797=ORIENTED_EDGE('',*,*,#2147,.T.);
#2798=ORIENTED_EDGE('',*,*,#2121,.T.);
#2799=ORIENTED_EDGE('',*,*,#2148,.T.);
#2800=ORIENTED_EDGE('',*,*,#2079,.T.);
#2801=ORIENTED_EDGE('',*,*,#2149,.T.);
#2802=ORIENTED_EDGE('',*,*,#2128,.T.);
#2803=ORIENTED_EDGE('',*,*,#2150,.T.);
#2804=ORIENTED_EDGE('',*,*,#2151,.F.);
#2805=ORIENTED_EDGE('',*,*,#2113,.T.);
#2806=ORIENTED_EDGE('',*,*,#2152,.F.);
#2807=ORIENTED_EDGE('',*,*,#2122,.T.);
#2808=ORIENTED_EDGE('',*,*,#2147,.F.);
#2809=ORIENTED_EDGE('',*,*,#2099,.T.);
#2810=ORIENTED_EDGE('',*,*,#2103,.T.);
#2811=ORIENTED_EDGE('',*,*,#2153,.F.);
#2812=ORIENTED_EDGE('',*,*,#2108,.T.);
#2813=ORIENTED_EDGE('',*,*,#2144,.F.);
#2814=ORIENTED_EDGE('',*,*,#2092,.T.);
#2815=ORIENTED_EDGE('',*,*,#2096,.T.);
#2816=ORIENTED_EDGE('',*,*,#2154,.F.);
#2817=ORIENTED_EDGE('',*,*,#2115,.T.);
#2818=ORIENTED_EDGE('',*,*,#2146,.F.);
#2819=ORIENTED_EDGE('',*,*,#2094,.T.);
#2820=ORIENTED_EDGE('',*,*,#2145,.F.);
#2821=ORIENTED_EDGE('',*,*,#2106,.T.);
#2822=ORIENTED_EDGE('',*,*,#2110,.T.);
#2823=ORIENTED_EDGE('',*,*,#2155,.F.);
#2824=ORIENTED_EDGE('',*,*,#2085,.T.);
#2825=ORIENTED_EDGE('',*,*,#2156,.F.);
#2826=ORIENTED_EDGE('',*,*,#2101,.T.);
#2827=ORIENTED_EDGE('',*,*,#2143,.F.);
#2828=ORIENTED_EDGE('',*,*,#2090,.T.);
#2829=ORIENTED_EDGE('',*,*,#2142,.F.);
#2830=ORIENTED_EDGE('',*,*,#2134,.T.);
#2831=ORIENTED_EDGE('',*,*,#2157,.F.);
#2832=ORIENTED_EDGE('',*,*,#2078,.T.);
#2833=ORIENTED_EDGE('',*,*,#2158,.F.);
#2834=ORIENTED_EDGE('',*,*,#2132,.T.);
#2835=ORIENTED_EDGE('',*,*,#2129,.T.);
#2836=ORIENTED_EDGE('',*,*,#2149,.F.);
#2837=ORIENTED_EDGE('',*,*,#2080,.T.);
#2838=ORIENTED_EDGE('',*,*,#2148,.F.);
#2839=ORIENTED_EDGE('',*,*,#2120,.T.);
#2840=ORIENTED_EDGE('',*,*,#2159,.F.);
#2841=ORIENTED_EDGE('',*,*,#2071,.T.);
#2842=ORIENTED_EDGE('',*,*,#2160,.F.);
#2843=ORIENTED_EDGE('',*,*,#2139,.T.);
#2844=ORIENTED_EDGE('',*,*,#2136,.T.);
#2845=ORIENTED_EDGE('',*,*,#2141,.F.);
#2846=ORIENTED_EDGE('',*,*,#2076,.T.);
#2847=ORIENTED_EDGE('',*,*,#2073,.T.);
#2848=ORIENTED_EDGE('',*,*,#2150,.F.);
#2849=ORIENTED_EDGE('',*,*,#2127,.T.);
#2850=ORIENTED_EDGE('',*,*,#2161,.F.);
#2851=ORIENTED_EDGE('',*,*,#2162,.F.);
#2852=ORIENTED_EDGE('',*,*,#2163,.T.);
#2853=ORIENTED_EDGE('',*,*,#2138,.T.);
#2854=ORIENTED_EDGE('',*,*,#2131,.T.);
#2855=ORIENTED_EDGE('',*,*,#2125,.T.);
#2856=ORIENTED_EDGE('',*,*,#2118,.T.);
#2857=ORIENTED_EDGE('',*,*,#2112,.T.);
#2858=ORIENTED_EDGE('',*,*,#2105,.T.);
#2859=ORIENTED_EDGE('',*,*,#2098,.T.);
#2860=ORIENTED_EDGE('',*,*,#2088,.T.);
#2861=ORIENTED_EDGE('',*,*,#2083,.T.);
#2862=ORIENTED_EDGE('',*,*,#2075,.T.);
#2863=ORIENTED_EDGE('',*,*,#2164,.F.);
#2864=ORIENTED_EDGE('',*,*,#2165,.T.);
#2865=ORIENTED_EDGE('',*,*,#2162,.T.);
#2866=ORIENTED_EDGE('',*,*,#2165,.F.);
#2867=ORIENTED_EDGE('',*,*,#2164,.T.);
#2868=ORIENTED_EDGE('',*,*,#2077,.T.);
#2869=ORIENTED_EDGE('',*,*,#2161,.T.);
#2870=ORIENTED_EDGE('',*,*,#2133,.T.);
#2871=ORIENTED_EDGE('',*,*,#2158,.T.);
#2872=ORIENTED_EDGE('',*,*,#2084,.T.);
#2873=ORIENTED_EDGE('',*,*,#2081,.T.);
#2874=ORIENTED_EDGE('',*,*,#2159,.T.);
#2875=ORIENTED_EDGE('',*,*,#2126,.T.);
#2876=ORIENTED_EDGE('',*,*,#2123,.T.);
#2877=ORIENTED_EDGE('',*,*,#2152,.T.);
#2878=ORIENTED_EDGE('',*,*,#2119,.T.);
#2879=ORIENTED_EDGE('',*,*,#2116,.T.);
#2880=ORIENTED_EDGE('',*,*,#2154,.T.);
#2881=ORIENTED_EDGE('',*,*,#2095,.T.);
#2882=ORIENTED_EDGE('',*,*,#2155,.T.);
#2883=ORIENTED_EDGE('',*,*,#2109,.T.);
#2884=ORIENTED_EDGE('',*,*,#2153,.T.);
#2885=ORIENTED_EDGE('',*,*,#2102,.T.);
#2886=ORIENTED_EDGE('',*,*,#2156,.T.);
#2887=ORIENTED_EDGE('',*,*,#2091,.T.);
#2888=ORIENTED_EDGE('',*,*,#2157,.T.);
#2889=ORIENTED_EDGE('',*,*,#2140,.T.);
#2890=ORIENTED_EDGE('',*,*,#2160,.T.);
#2891=ORIENTED_EDGE('',*,*,#2151,.T.);
#2892=ORIENTED_EDGE('',*,*,#2166,.T.);
#2893=ORIENTED_EDGE('',*,*,#2163,.F.);
#2894=ORIENTED_EDGE('',*,*,#2166,.F.);
#3448=CYLINDRICAL_SURFACE('',#4090,0.22);
#3449=CYLINDRICAL_SURFACE('',#4094,0.22);
#3450=CYLINDRICAL_SURFACE('',#4099,0.22);
#3451=CYLINDRICAL_SURFACE('',#4104,0.22);
#3452=CYLINDRICAL_SURFACE('',#4108,0.22);
#3453=CYLINDRICAL_SURFACE('',#4112,0.22);
#3454=CYLINDRICAL_SURFACE('',#4116,0.22);
#3455=CYLINDRICAL_SURFACE('',#4121,0.22);
#3456=CYLINDRICAL_SURFACE('',#4126,0.22);
#3457=CYLINDRICAL_SURFACE('',#4130,0.22);
#3458=CYLINDRICAL_SURFACE('',#4169,1.4);
#3459=CYLINDRICAL_SURFACE('',#4172,0.8);
#3540=ADVANCED_FACE('',(#569),#3448,.F.);
#3541=ADVANCED_FACE('',(#570),#3449,.F.);
#3542=ADVANCED_FACE('',(#571),#3450,.F.);
#3543=ADVANCED_FACE('',(#572),#3451,.F.);
#3544=ADVANCED_FACE('',(#573),#3452,.F.);
#3545=ADVANCED_FACE('',(#574),#3453,.F.);
#3546=ADVANCED_FACE('',(#575),#3454,.F.);
#3547=ADVANCED_FACE('',(#576),#3455,.F.);
#3548=ADVANCED_FACE('',(#577),#3456,.F.);
#3549=ADVANCED_FACE('',(#578),#3457,.F.);
#3550=ADVANCED_FACE('',(#579,#395),#452,.T.);
#3551=ADVANCED_FACE('',(#580),#180,.F.);
#3552=ADVANCED_FACE('',(#581),#181,.F.);
#3553=ADVANCED_FACE('',(#582),#182,.F.);
#3554=ADVANCED_FACE('',(#583),#183,.F.);
#3555=ADVANCED_FACE('',(#584),#184,.F.);
#3556=ADVANCED_FACE('',(#585),#185,.F.);
#3557=ADVANCED_FACE('',(#586),#186,.F.);
#3558=ADVANCED_FACE('',(#587),#187,.F.);
#3559=ADVANCED_FACE('',(#588),#188,.F.);
#3560=ADVANCED_FACE('',(#589),#189,.F.);
#3561=ADVANCED_FACE('',(#590,#396,#397,#398,#399,#400,#401,#402,#403,#404,
#405,#406),#453,.T.);
#3562=ADVANCED_FACE('',(#591),#3458,.T.);
#3563=ADVANCED_FACE('',(#592,#407),#454,.T.);
#3564=ADVANCED_FACE('',(#593),#3459,.F.);
#3707=CLOSED_SHELL('',(#3540,#3541,#3542,#3543,#3544,#3545,#3546,#3547,
#3548,#3549,#3550,#3551,#3552,#3553,#3554,#3555,#3556,#3557,#3558,#3559,
#3560,#3561,#3562,#3563,#3564));
#4089=AXIS2_PLACEMENT_3D('',#6292,#4776,#4777);
#4090=AXIS2_PLACEMENT_3D('',#6293,#4778,#4779);
#4091=AXIS2_PLACEMENT_3D('',#6313,#4780,#4781);
#4092=AXIS2_PLACEMENT_3D('',#6325,#4783,#4784);
#4093=AXIS2_PLACEMENT_3D('',#6339,#4785,#4786);
#4094=AXIS2_PLACEMENT_3D('',#6340,#4787,#4788);
#4095=AXIS2_PLACEMENT_3D('',#6360,#4789,#4790);
#4096=AXIS2_PLACEMENT_3D('',#6379,#4791,#4792);
#4097=AXIS2_PLACEMENT_3D('',#6382,#4794,#4795);
#4098=AXIS2_PLACEMENT_3D('',#6383,#4796,#4797);
#4099=AXIS2_PLACEMENT_3D('',#6384,#4798,#4799);
#4100=AXIS2_PLACEMENT_3D('',#6404,#4800,#4801);
#4101=AXIS2_PLACEMENT_3D('',#6407,#4803,#4804);
#4102=AXIS2_PLACEMENT_3D('',#6409,#4805,#4806);
#4103=AXIS2_PLACEMENT_3D('',#6427,#4807,#4808);
#4104=AXIS2_PLACEMENT_3D('',#6428,#4809,#4810);
#4105=AXIS2_PLACEMENT_3D('',#6446,#4811,#4812);
#4106=AXIS2_PLACEMENT_3D('',#6465,#4813,#4814);
#4107=AXIS2_PLACEMENT_3D('',#6474,#4816,#4817);
#4108=AXIS2_PLACEMENT_3D('',#6475,#4818,#4819);
#4109=AXIS2_PLACEMENT_3D('',#6483,#4820,#4821);
#4110=AXIS2_PLACEMENT_3D('',#6502,#4822,#4823);
#4111=AXIS2_PLACEMENT_3D('',#6521,#4825,#4826);
#4112=AXIS2_PLACEMENT_3D('',#6522,#4827,#4828);
#4113=AXIS2_PLACEMENT_3D('',#6536,#4829,#4830);
#4114=AXIS2_PLACEMENT_3D('',#6555,#4831,#4832);
#4115=AXIS2_PLACEMENT_3D('',#6568,#4834,#4835);
#4116=AXIS2_PLACEMENT_3D('',#6569,#4836,#4837);
#4117=AXIS2_PLACEMENT_3D('',#6589,#4838,#4839);
#4118=AXIS2_PLACEMENT_3D('',#6608,#4840,#4841);
#4119=AXIS2_PLACEMENT_3D('',#6611,#4843,#4844);
#4120=AXIS2_PLACEMENT_3D('',#6612,#4845,#4846);
#4121=AXIS2_PLACEMENT_3D('',#6613,#4847,#4848);
#4122=AXIS2_PLACEMENT_3D('',#6633,#4849,#4850);
#4123=AXIS2_PLACEMENT_3D('',#6652,#4851,#4852);
#4124=AXIS2_PLACEMENT_3D('',#6655,#4854,#4855);
#4125=AXIS2_PLACEMENT_3D('',#6656,#4856,#4857);
#4126=AXIS2_PLACEMENT_3D('',#6657,#4858,#4859);
#4127=AXIS2_PLACEMENT_3D('',#6677,#4860,#4861);
#4128=AXIS2_PLACEMENT_3D('',#6693,#4863,#4864);
#4129=AXIS2_PLACEMENT_3D('',#6703,#4865,#4866);
#4130=AXIS2_PLACEMENT_3D('',#6704,#4867,#4868);
#4131=AXIS2_PLACEMENT_3D('',#6724,#4869,#4870);
#4132=AXIS2_PLACEMENT_3D('',#6732,#4872,#4873);
#4133=AXIS2_PLACEMENT_3D('',#6750,#4874,#4875);
#4134=AXIS2_PLACEMENT_3D('',#6751,#4876,#4877);
#4135=AXIS2_PLACEMENT_3D('',#6752,#4878,#4879);
#4136=AXIS2_PLACEMENT_3D('',#6753,#4880,#4881);
#4137=AXIS2_PLACEMENT_3D('',#6754,#4882,#4883);
#4138=AXIS2_PLACEMENT_3D('',#6755,#4884,#4885);
#4139=AXIS2_PLACEMENT_3D('',#6756,#4886,#4887);
#4140=AXIS2_PLACEMENT_3D('',#6757,#4888,#4889);
#4141=AXIS2_PLACEMENT_3D('',#6758,#4890,#4891);
#4142=AXIS2_PLACEMENT_3D('',#6759,#4892,#4893);
#4143=AXIS2_PLACEMENT_3D('',#6760,#4894,#4895);
#4144=AXIS2_PLACEMENT_3D('',#6761,#4896,#4897);
#4145=AXIS2_PLACEMENT_3D('',#6763,#4898,#4899);
#4146=AXIS2_PLACEMENT_3D('',#6764,#4900,#4901);
#4147=AXIS2_PLACEMENT_3D('',#6765,#4902,#4903);
#4148=AXIS2_PLACEMENT_3D('',#6766,#4904,#4905);
#4149=AXIS2_PLACEMENT_3D('',#6767,#4906,#4907);
#4150=AXIS2_PLACEMENT_3D('',#6768,#4908,#4909);
#4151=AXIS2_PLACEMENT_3D('',#6769,#4910,#4911);
#4152=AXIS2_PLACEMENT_3D('',#6770,#4912,#4913);
#4153=AXIS2_PLACEMENT_3D('',#6771,#4914,#4915);
#4154=AXIS2_PLACEMENT_3D('',#6772,#4916,#4917);
#4155=AXIS2_PLACEMENT_3D('',#6773,#4918,#4919);
#4156=AXIS2_PLACEMENT_3D('',#6774,#4920,#4921);
#4157=AXIS2_PLACEMENT_3D('',#6775,#4922,#4923);
#4158=AXIS2_PLACEMENT_3D('',#6776,#4924,#4925);
#4159=AXIS2_PLACEMENT_3D('',#6777,#4926,#4927);
#4160=AXIS2_PLACEMENT_3D('',#6778,#4928,#4929);
#4161=AXIS2_PLACEMENT_3D('',#6779,#4930,#4931);
#4162=AXIS2_PLACEMENT_3D('',#6780,#4932,#4933);
#4163=AXIS2_PLACEMENT_3D('',#6781,#4934,#4935);
#4164=AXIS2_PLACEMENT_3D('',#6782,#4936,#4937);
#4165=AXIS2_PLACEMENT_3D('',#6783,#4938,#4939);
#4166=AXIS2_PLACEMENT_3D('',#6784,#4940,#4941);
#4167=AXIS2_PLACEMENT_3D('',#6786,#4942,#4943);
#4168=AXIS2_PLACEMENT_3D('',#6788,#4944,#4945);
#4169=AXIS2_PLACEMENT_3D('',#6789,#4946,#4947);
#4170=AXIS2_PLACEMENT_3D('',#6791,#4948,#4949);
#4171=AXIS2_PLACEMENT_3D('',#6793,#4951,#4952);
#4172=AXIS2_PLACEMENT_3D('',#6794,#4953,#4954);
#4776=DIRECTION('axis',(0.,0.,1.));
#4777=DIRECTION('refdir',(1.,0.,0.));
#4778=DIRECTION('center_axis',(0.,1.,0.));
#4779=DIRECTION('ref_axis',(1.,0.,0.));
#4780=DIRECTION('center_axis',(0.,1.,0.));
#4781=DIRECTION('ref_axis',(1.,0.,0.));
#4782=DIRECTION('',(0.,1.,0.));
#4783=DIRECTION('center_axis',(0.,-1.,0.));
#4784=DIRECTION('ref_axis',(1.,0.,0.));
#4785=DIRECTION('center_axis',(0.,1.,0.));
#4786=DIRECTION('ref_axis',(1.,0.,0.));
#4787=DIRECTION('center_axis',(0.,1.,0.));
#4788=DIRECTION('ref_axis',(1.,0.,0.));
#4789=DIRECTION('center_axis',(0.,1.,0.));
#4790=DIRECTION('ref_axis',(1.,0.,0.));
#4791=DIRECTION('center_axis',(0.,1.,0.));
#4792=DIRECTION('ref_axis',(1.,0.,0.));
#4793=DIRECTION('',(0.,1.,0.));
#4794=DIRECTION('center_axis',(0.,-1.,0.));
#4795=DIRECTION('ref_axis',(1.,0.,0.));
#4796=DIRECTION('center_axis',(0.,1.,0.));
#4797=DIRECTION('ref_axis',(1.,0.,0.));
#4798=DIRECTION('center_axis',(0.,1.,0.));
#4799=DIRECTION('ref_axis',(1.,0.,0.));
#4800=DIRECTION('center_axis',(0.,1.,0.));
#4801=DIRECTION('ref_axis',(1.,0.,0.));
#4802=DIRECTION('',(0.,1.,0.));
#4803=DIRECTION('center_axis',(0.,-1.,0.));
#4804=DIRECTION('ref_axis',(1.,0.,0.));
#4805=DIRECTION('center_axis',(0.,1.,0.));
#4806=DIRECTION('ref_axis',(1.,0.,0.));
#4807=DIRECTION('center_axis',(0.,1.,0.));
#4808=DIRECTION('ref_axis',(1.,0.,0.));
#4809=DIRECTION('center_axis',(0.,1.,0.));
#4810=DIRECTION('ref_axis',(1.,0.,0.));
#4811=DIRECTION('center_axis',(0.,1.,0.));
#4812=DIRECTION('ref_axis',(1.,0.,0.));
#4813=DIRECTION('center_axis',(0.,1.,0.));
#4814=DIRECTION('ref_axis',(1.,0.,0.));
#4815=DIRECTION('',(0.,1.,0.));
#4816=DIRECTION('center_axis',(0.,-1.,0.));
#4817=DIRECTION('ref_axis',(1.,0.,0.));
#4818=DIRECTION('center_axis',(0.,1.,0.));
#4819=DIRECTION('ref_axis',(1.,0.,0.));
#4820=DIRECTION('center_axis',(0.,1.,0.));
#4821=DIRECTION('ref_axis',(1.,0.,0.));
#4822=DIRECTION('center_axis',(0.,1.,0.));
#4823=DIRECTION('ref_axis',(1.,0.,0.));
#4824=DIRECTION('',(0.,1.,0.));
#4825=DIRECTION('center_axis',(0.,-1.,0.));
#4826=DIRECTION('ref_axis',(1.,0.,0.));
#4827=DIRECTION('center_axis',(0.,1.,0.));
#4828=DIRECTION('ref_axis',(1.,0.,0.));
#4829=DIRECTION('center_axis',(0.,1.,0.));
#4830=DIRECTION('ref_axis',(1.,0.,0.));
#4831=DIRECTION('center_axis',(0.,1.,0.));
#4832=DIRECTION('ref_axis',(1.,0.,0.));
#4833=DIRECTION('',(0.,1.,0.));
#4834=DIRECTION('center_axis',(0.,-1.,0.));
#4835=DIRECTION('ref_axis',(1.,0.,0.));
#4836=DIRECTION('center_axis',(0.,1.,0.));
#4837=DIRECTION('ref_axis',(1.,0.,0.));
#4838=DIRECTION('center_axis',(0.,1.,0.));
#4839=DIRECTION('ref_axis',(1.,0.,0.));
#4840=DIRECTION('center_axis',(0.,1.,0.));
#4841=DIRECTION('ref_axis',(1.,0.,0.));
#4842=DIRECTION('',(0.,1.,0.));
#4843=DIRECTION('center_axis',(0.,-1.,0.));
#4844=DIRECTION('ref_axis',(1.,0.,0.));
#4845=DIRECTION('center_axis',(0.,1.,0.));
#4846=DIRECTION('ref_axis',(1.,0.,0.));
#4847=DIRECTION('center_axis',(0.,1.,0.));
#4848=DIRECTION('ref_axis',(1.,0.,0.));
#4849=DIRECTION('center_axis',(0.,1.,0.));
#4850=DIRECTION('ref_axis',(1.,0.,0.));
#4851=DIRECTION('center_axis',(0.,1.,0.));
#4852=DIRECTION('ref_axis',(1.,0.,0.));
#4853=DIRECTION('',(0.,1.,0.));
#4854=DIRECTION('center_axis',(0.,-1.,0.));
#4855=DIRECTION('ref_axis',(1.,0.,0.));
#4856=DIRECTION('center_axis',(0.,1.,0.));
#4857=DIRECTION('ref_axis',(1.,0.,0.));
#4858=DIRECTION('center_axis',(0.,1.,0.));
#4859=DIRECTION('ref_axis',(1.,0.,0.));
#4860=DIRECTION('center_axis',(0.,1.,0.));
#4861=DIRECTION('ref_axis',(1.,0.,0.));
#4862=DIRECTION('',(0.,1.,0.));
#4863=DIRECTION('center_axis',(0.,-1.,0.));
#4864=DIRECTION('ref_axis',(1.,0.,0.));
#4865=DIRECTION('center_axis',(0.,1.,0.));
#4866=DIRECTION('ref_axis',(1.,0.,0.));
#4867=DIRECTION('center_axis',(0.,1.,0.));
#4868=DIRECTION('ref_axis',(1.,0.,0.));
#4869=DIRECTION('center_axis',(0.,1.,0.));
#4870=DIRECTION('ref_axis',(1.,0.,0.));
#4871=DIRECTION('',(0.,1.,0.));
#4872=DIRECTION('center_axis',(0.,-1.,0.));
#4873=DIRECTION('ref_axis',(1.,0.,0.));
#4874=DIRECTION('center_axis',(0.,1.,0.));
#4875=DIRECTION('ref_axis',(1.,0.,0.));
#4876=DIRECTION('center_axis',(0.,-1.,0.));
#4877=DIRECTION('ref_axis',(0.,0.,-1.));
#4878=DIRECTION('center_axis',(0.,-1.,0.));
#4879=DIRECTION('ref_axis',(0.,0.,-1.));
#4880=DIRECTION('center_axis',(0.,-1.,0.));
#4881=DIRECTION('ref_axis',(0.,0.,-1.));
#4882=DIRECTION('center_axis',(0.,-1.,0.));
#4883=DIRECTION('ref_axis',(0.,0.,-1.));
#4884=DIRECTION('center_axis',(0.,-1.,0.));
#4885=DIRECTION('ref_axis',(0.,0.,-1.));
#4886=DIRECTION('center_axis',(0.,-1.,0.));
#4887=DIRECTION('ref_axis',(0.,0.,-1.));
#4888=DIRECTION('center_axis',(0.,-1.,0.));
#4889=DIRECTION('ref_axis',(0.,0.,-1.));
#4890=DIRECTION('center_axis',(0.,-1.,0.));
#4891=DIRECTION('ref_axis',(0.,0.,-1.));
#4892=DIRECTION('center_axis',(0.,-1.,0.));
#4893=DIRECTION('ref_axis',(0.,0.,-1.));
#4894=DIRECTION('center_axis',(0.,-1.,0.));
#4895=DIRECTION('ref_axis',(0.,0.,-1.));
#4896=DIRECTION('center_axis',(0.,-1.,0.));
#4897=DIRECTION('ref_axis',(0.,0.,-1.));
#4898=DIRECTION('center_axis',(0.,-1.,0.));
#4899=DIRECTION('ref_axis',(1.,0.,0.));
#4900=DIRECTION('center_axis',(0.,-1.,0.));
#4901=DIRECTION('ref_axis',(0.,0.,-1.));
#4902=DIRECTION('center_axis',(0.,1.,0.));
#4903=DIRECTION('ref_axis',(0.,0.,-1.));
#4904=DIRECTION('center_axis',(0.,-1.,0.));
#4905=DIRECTION('ref_axis',(0.,0.,-1.));
#4906=DIRECTION('center_axis',(0.,1.,0.));
#4907=DIRECTION('ref_axis',(0.,0.,-1.));
#4908=DIRECTION('center_axis',(0.,-1.,0.));
#4909=DIRECTION('ref_axis',(0.,0.,-1.));
#4910=DIRECTION('center_axis',(0.,1.,0.));
#4911=DIRECTION('ref_axis',(0.,0.,-1.));
#4912=DIRECTION('center_axis',(0.,-1.,0.));
#4913=DIRECTION('ref_axis',(-1.22464679914735E-16,0.,1.));
#4914=DIRECTION('center_axis',(0.,1.,0.));
#4915=DIRECTION('ref_axis',(0.,0.,-1.));
#4916=DIRECTION('center_axis',(0.,-1.,0.));
#4917=DIRECTION('ref_axis',(0.,0.,-1.));
#4918=DIRECTION('center_axis',(0.,1.,0.));
#4919=DIRECTION('ref_axis',(0.,0.,-1.));
#4920=DIRECTION('center_axis',(0.,-1.,0.));
#4921=DIRECTION('ref_axis',(0.,0.,-1.));
#4922=DIRECTION('center_axis',(0.,1.,0.));
#4923=DIRECTION('ref_axis',(0.,0.,-1.));
#4924=DIRECTION('center_axis',(0.,-1.,0.));
#4925=DIRECTION('ref_axis',(0.,0.,-1.));
#4926=DIRECTION('center_axis',(0.,1.,0.));
#4927=DIRECTION('ref_axis',(0.,0.,-1.));
#4928=DIRECTION('center_axis',(0.,-1.,0.));
#4929=DIRECTION('ref_axis',(0.,0.,-1.));
#4930=DIRECTION('center_axis',(0.,1.,0.));
#4931=DIRECTION('ref_axis',(0.,0.,-1.));
#4932=DIRECTION('center_axis',(0.,-1.,0.));
#4933=DIRECTION('ref_axis',(0.,0.,-1.));
#4934=DIRECTION('center_axis',(0.,1.,0.));
#4935=DIRECTION('ref_axis',(0.,0.,-1.));
#4936=DIRECTION('center_axis',(0.,-1.,0.));
#4937=DIRECTION('ref_axis',(0.,0.,-1.));
#4938=DIRECTION('center_axis',(0.,1.,0.));
#4939=DIRECTION('ref_axis',(0.,0.,-1.));
#4940=DIRECTION('center_axis',(0.,1.,0.));
#4941=DIRECTION('ref_axis',(0.,0.,1.));
#4942=DIRECTION('center_axis',(0.,-1.,0.));
#4943=DIRECTION('ref_axis',(1.,0.,0.));
#4944=DIRECTION('center_axis',(0.,-1.,0.));
#4945=DIRECTION('ref_axis',(1.,0.,0.));
#4946=DIRECTION('center_axis',(0.,-1.,0.));
#4947=DIRECTION('ref_axis',(1.,0.,0.));
#4948=DIRECTION('center_axis',(0.,-1.,0.));
#4949=DIRECTION('ref_axis',(1.,0.,0.));
#4950=DIRECTION('',(0.,1.,0.));
#4951=DIRECTION('center_axis',(0.,-1.,0.));
#4952=DIRECTION('ref_axis',(0.,0.,-1.));
#4953=DIRECTION('center_axis',(0.,-1.,0.));
#4954=DIRECTION('ref_axis',(1.,0.,0.));
#4955=DIRECTION('',(0.,1.,0.));
#6292=CARTESIAN_POINT('',(0.,0.,0.));
#6293=CARTESIAN_POINT('Origin',(0.339918693812442,0.,-1.04616216792467));
#6294=CARTESIAN_POINT('',(0.388099915049348,0.55,-0.831502973106184));
#6295=CARTESIAN_POINT('',(0.52031818912536,0.55,-1.17208286555157));
#6296=CARTESIAN_POINT('Ctrl Pts',(0.388099915049348,0.55,-0.831502973106184));
#6297=CARTESIAN_POINT('Ctrl Pts',(0.400811235892708,0.564520591324654,-0.83435608621082));
#6298=CARTESIAN_POINT('Ctrl Pts',(0.414489441774858,0.578350901074076,-0.838641228510082));
#6299=CARTESIAN_POINT('Ctrl Pts',(0.442060797330418,0.603582622702572,-0.85072830691315));
#6300=CARTESIAN_POINT('Ctrl Pts',(0.456158463572915,0.615143118816555,-0.858605324728243));
#6301=CARTESIAN_POINT('Ctrl Pts',(0.484752922098353,0.635707573307249,-0.879540531101799));
#6302=CARTESIAN_POINT('Ctrl Pts',(0.499051049160274,0.644312375876114,-0.892876836196423));
#6303=CARTESIAN_POINT('Ctrl Pts',(0.52379576928235,0.655446685849628,-0.923864041185002));
#6304=CARTESIAN_POINT('Ctrl Pts',(0.533985305944486,0.658130838683679,-0.940643830369111));
#6305=CARTESIAN_POINT('Ctrl Pts',(0.550361643571044,0.657849180985917,-0.9785497830379));
#6306=CARTESIAN_POINT('Ctrl Pts',(0.555779214799253,0.654458884420129,-0.998971235859073));
#6307=CARTESIAN_POINT('Ctrl Pts',(0.561389818753197,0.64103073977944,-1.04471484600978));
#6308=CARTESIAN_POINT('Ctrl Pts',(0.559917035408428,0.629849556228346,-1.06921795983998));
#6309=CARTESIAN_POINT('Ctrl Pts',(0.548343966268834,0.597265816764751,-1.12384601890666));
#6310=CARTESIAN_POINT('Ctrl Pts',(0.534981138426803,0.574166902399579,-1.15107608347657));
#6311=CARTESIAN_POINT('Ctrl Pts',(0.52031818912536,0.55,-1.17208286555157));
#6312=CARTESIAN_POINT('',(0.174765758038764,0.55,-0.900819442598166));
#6313=CARTESIAN_POINT('Origin',(0.339918693812442,0.55,-1.04616216792467));
#6314=CARTESIAN_POINT('',(0.119918693812442,0.652623283223421,-1.04616216792467));
#6315=CARTESIAN_POINT('Ctrl Pts',(0.119918693812442,0.652623283223421,-1.04616216792467));
#6316=CARTESIAN_POINT('Ctrl Pts',(0.119918693812442,0.651548657113519,-1.04149771220363));
#6317=CARTESIAN_POINT('Ctrl Pts',(0.120067055145305,0.650315309709256,-1.03685410010078));
#6318=CARTESIAN_POINT('Ctrl Pts',(0.12183667592796,0.64191056343947,-1.00894801471422));
#6319=CARTESIAN_POINT('Ctrl Pts',(0.126905360909727,0.631232140955599,-0.987436230688157));
#6320=CARTESIAN_POINT('Ctrl Pts',(0.14498964584378,0.598578363965738,-0.939719972286296));
#6321=CARTESIAN_POINT('Ctrl Pts',(0.160293285605306,0.574417013842143,-0.917264512724103));
#6322=CARTESIAN_POINT('Ctrl Pts',(0.174765758038763,0.55,-0.900819442598166));
#6323=CARTESIAN_POINT('',(0.119918693812442,0.9,-1.04616216792467));
#6324=CARTESIAN_POINT('',(0.119918693812442,0.,-1.04616216792467));
#6325=CARTESIAN_POINT('Origin',(0.339918693812442,0.9,-1.04616216792467));
#6326=CARTESIAN_POINT('',(0.267986765351098,0.55,-1.25407031511432));
#6327=CARTESIAN_POINT('Ctrl Pts',(0.267986765351098,0.55,-1.25407031511432));
#6328=CARTESIAN_POINT('Ctrl Pts',(0.253293148857989,0.564667428121554,-1.24898662703038));
#6329=CARTESIAN_POINT('Ctrl Pts',(0.238057625599671,0.578482229661416,-1.2419316754898));
#6330=CARTESIAN_POINT('Ctrl Pts',(0.208963044113739,0.603467206297433,-1.22375112901188));
#6331=CARTESIAN_POINT('Ctrl Pts',(0.194942594271843,0.614783224033247,-1.21267059279651));
#6332=CARTESIAN_POINT('Ctrl Pts',(0.167829116505891,0.635319330100661,-1.18473227113195));
#6333=CARTESIAN_POINT('Ctrl Pts',(0.155029153917438,0.644168216758556,-1.16745023332297));
#6334=CARTESIAN_POINT('Ctrl Pts',(0.135809963569082,0.655254671849834,-1.13051582480638));
#6335=CARTESIAN_POINT('Ctrl Pts',(0.129007044228756,0.658058624819753,-1.11187531830365));
#6336=CARTESIAN_POINT('Ctrl Pts',(0.121501840920505,0.657952259751555,-1.07686180187776));
#6337=CARTESIAN_POINT('Ctrl Pts',(0.119918693812442,0.656134080516753,-1.06140091782046));
#6338=CARTESIAN_POINT('Ctrl Pts',(0.119918693812442,0.652623283223421,-1.04616216792467));
#6339=CARTESIAN_POINT('Origin',(0.339918693812442,0.55,-1.04616216792467));
#6340=CARTESIAN_POINT('Origin',(-0.889918693812442,0.,-0.64656377752172));
#6341=CARTESIAN_POINT('',(-0.670876851625708,0.55,-0.626053502744384));
#6342=CARTESIAN_POINT('',(-0.953929883998579,0.55,-0.857045528585688));
#6343=CARTESIAN_POINT('Ctrl Pts',(-0.670876851625708,0.55,-0.626053502744384));
#6344=CARTESIAN_POINT('Ctrl Pts',(-0.669661497485836,0.564530296745674,
-0.639033017285112));
#6345=CARTESIAN_POINT('Ctrl Pts',(-0.669510740703862,0.578369513099121,
-0.653376521307855));
#6346=CARTESIAN_POINT('Ctrl Pts',(-0.672482969531502,0.603533376354093,
-0.68325868771487));
#6347=CARTESIAN_POINT('Ctrl Pts',(-0.675592903940688,0.615031149045687,
-0.699004528749127));
#6348=CARTESIAN_POINT('Ctrl Pts',(-0.686609461544843,0.635610628918897,
-0.732627526493686));
#6349=CARTESIAN_POINT('Ctrl Pts',(-0.694884092102898,0.644260777278176,
-0.750408507220998));
#6350=CARTESIAN_POINT('Ctrl Pts',(-0.716725112096974,0.655427509796643,
-0.783571551911549));
#6351=CARTESIAN_POINT('Ctrl Pts',(-0.729520363220727,0.65812029334222,-0.798445101607854));
#6352=CARTESIAN_POINT('Ctrl Pts',(-0.760487823778074,0.657862066752901,
-0.825743319709736));
#6353=CARTESIAN_POINT('Ctrl Pts',(-0.778230186437556,0.654483119781693,
-0.837216662588005));
#6354=CARTESIAN_POINT('Ctrl Pts',(-0.820018109421027,0.641069161130152,
-0.856722945878246));
#6355=CARTESIAN_POINT('Ctrl Pts',(-0.843800606133157,0.629882880868174,
-0.862908527531438));
#6356=CARTESIAN_POINT('Ctrl Pts',(-0.899368376134036,0.597285070273299,
-0.868796870135415));
#6357=CARTESIAN_POINT('Ctrl Pts',(-0.92940946533079,0.574177434161681,-0.864502617738803));
#6358=CARTESIAN_POINT('Ctrl Pts',(-0.95392988399858,0.55,-0.857045528585688));
#6359=CARTESIAN_POINT('',(-0.802724611619556,0.55,-0.444580629634229));
#6360=CARTESIAN_POINT('Origin',(-0.889918693812442,0.55,-0.64656377752172));
#6361=CARTESIAN_POINT('',(-1.10987928032073,0.55,-0.642399598979491));
#6362=CARTESIAN_POINT('Ctrl Pts',(-1.10987928032073,0.55,-0.642399598979491));
#6363=CARTESIAN_POINT('Ctrl Pts',(-1.10958615470441,0.564609024168173,-0.626916093209465));
#6364=CARTESIAN_POINT('Ctrl Pts',(-1.10759949863652,0.57837155464205,-0.610317305256214));
#6365=CARTESIAN_POINT('Ctrl Pts',(-1.09937906630242,0.603238798649671,-0.577213727602755));
#6366=CARTESIAN_POINT('Ctrl Pts',(-1.09324919553707,0.614494006479294,-0.5605724935452));
#6367=CARTESIAN_POINT('Ctrl Pts',(-1.07518267284658,0.635086936255166,-0.526160358808756));
#6368=CARTESIAN_POINT('Ctrl Pts',(-1.06268941040781,0.644016986499168,-0.508543409408808));
#6369=CARTESIAN_POINT('Ctrl Pts',(-1.03345553095711,0.655200788127591,-0.478711490622469));
#6370=CARTESIAN_POINT('Ctrl Pts',(-1.0178159360962,0.658037254761758,-0.466436266197514));
#6371=CARTESIAN_POINT('Ctrl Pts',(-0.982652377717061,0.657961095551765,
-0.446004761419876));
#6372=CARTESIAN_POINT('Ctrl Pts',(-0.963865544104577,0.654904186336904,
-0.438426323310487));
#6373=CARTESIAN_POINT('Ctrl Pts',(-0.922132837036694,0.642003792826706,
-0.427684817450471));
#6374=CARTESIAN_POINT('Ctrl Pts',(-0.900086381736092,0.631337654594768,
-0.425835547406595));
#6375=CARTESIAN_POINT('Ctrl Pts',(-0.84902407335286,0.598671631847171,-0.428254106385369));
#6376=CARTESIAN_POINT('Ctrl Pts',(-0.822877500049853,0.574466130169061,
-0.435880831514466));
#6377=CARTESIAN_POINT('Ctrl Pts',(-0.802724611619556,0.55,-0.444580629634229));
#6378=CARTESIAN_POINT('',(-1.10991869381244,0.55,-0.64656377752172));
#6379=CARTESIAN_POINT('Origin',(-0.889918693812442,0.55,-0.64656377752172));
#6380=CARTESIAN_POINT('',(-1.10991869381244,0.9,-0.64656377752172));
#6381=CARTESIAN_POINT('',(-1.10991869381244,0.,-0.64656377752172));
#6382=CARTESIAN_POINT('Origin',(-0.889918693812442,0.9,-0.64656377752172));
#6383=CARTESIAN_POINT('Origin',(-0.889918693812442,0.55,-0.64656377752172));
#6384=CARTESIAN_POINT('Origin',(1.1,0.,0.));
#6385=CARTESIAN_POINT('',(0.910735790157152,0.55,0.112156403618172));
#6386=CARTESIAN_POINT('',(1.27550420984285,0.55,0.132658480043447));
#6387=CARTESIAN_POINT('Ctrl Pts',(0.910735790157152,0.55,0.112156403618172));
#6388=CARTESIAN_POINT('Ctrl Pts',(0.917376089752458,0.564517997495034,0.123361925688083));
#6389=CARTESIAN_POINT('Ctrl Pts',(0.925676503375737,0.578345926844045,0.135044303040797));
#6390=CARTESIAN_POINT('Ctrl Pts',(0.945705763566752,0.603597412340976,0.157548233557299));
#6391=CARTESIAN_POINT('Ctrl Pts',(0.957575956315956,0.615176011910307,0.168539952403237));
#6392=CARTESIAN_POINT('Ctrl Pts',(0.986343324120607,0.635735932391,0.189265250815529));
#6393=CARTESIAN_POINT('Ctrl Pts',(1.00343254919411,0.644327528980788,0.198729556237649));
#6394=CARTESIAN_POINT('Ctrl Pts',(1.04053658704398,0.65545235887726,0.21267781162389));
#6395=CARTESIAN_POINT('Ctrl Pts',(1.05964780090184,0.658133955563747,0.217181471497843));
#6396=CARTESIAN_POINT('Ctrl Pts',(1.1007627783985,0.657845346648502,0.221036398352684));
#6397=CARTESIAN_POINT('Ctrl Pts',(1.12185832284616,0.65445169739566,0.219874810080966));
#6398=CARTESIAN_POINT('Ctrl Pts',(1.16708666484378,0.641019397008994,0.211069922924208));
#6399=CARTESIAN_POINT('Ctrl Pts',(1.18992721371268,0.629839760817717,0.202098025620397));
#6400=CARTESIAN_POINT('Ctrl Pts',(1.23829403807689,0.597260212402137,0.174213524003119));
#6401=CARTESIAN_POINT('Ctrl Pts',(1.2600586328202,0.574163836961989,0.153092633895046));
#6402=CARTESIAN_POINT('Ctrl Pts',(1.27550420984285,0.55,0.132658480043447));
#6403=CARTESIAN_POINT('',(0.88,0.55,2.69422295812418E-17));
#6404=CARTESIAN_POINT('Origin',(1.1,0.55,0.));
#6405=CARTESIAN_POINT('',(0.88,0.9,2.69422295812418E-17));
#6406=CARTESIAN_POINT('',(0.88,0.,2.69422295812418E-17));
#6407=CARTESIAN_POINT('Origin',(1.1,0.9,0.));
#6408=CARTESIAN_POINT('',(0.910735790157152,0.55,-0.112156403618172));
#6409=CARTESIAN_POINT('Origin',(1.1,0.55,0.));
#6410=CARTESIAN_POINT('',(1.27550420984285,0.55,-0.132658480043447));
#6411=CARTESIAN_POINT('Ctrl Pts',(1.27550420984285,0.55,-0.132658480043447));
#6412=CARTESIAN_POINT('Ctrl Pts',(1.26611782177473,0.56468453723726,-0.145076462072448));
#6413=CARTESIAN_POINT('Ctrl Pts',(1.25468431627751,0.578514647841062,-0.157400492027332));
#6414=CARTESIAN_POINT('Ctrl Pts',(1.22835219222699,0.603533958896828,-0.179483010322185));
#6415=CARTESIAN_POINT('Ctrl Pts',(1.21344338101808,0.614867643252025,-0.189407731207313));
#6416=CARTESIAN_POINT('Ctrl Pts',(1.17846267135551,0.635387178695068,-0.206540975098487));
#6417=CARTESIAN_POINT('Ctrl Pts',(1.15809147022147,0.644212495667266,-0.213351934557227));
#6418=CARTESIAN_POINT('Ctrl Pts',(1.11706033563968,0.65527050791581,-0.220191916744403));
#6419=CARTESIAN_POINT('Ctrl Pts',(1.09724086630217,0.658064897233583,-0.220893276198431));
#6420=CARTESIAN_POINT('Ctrl Pts',(1.05683477389847,0.657931008613642,-0.216703862540943));
#6421=CARTESIAN_POINT('Ctrl Pts',(1.03718465931368,0.654841874466928,-0.211762979306541));
#6422=CARTESIAN_POINT('Ctrl Pts',(0.997159417898573,0.641882889790503,-0.195877882014933));
#6423=CARTESIAN_POINT('Ctrl Pts',(0.978275892037171,0.631200912596756,-0.184408191234793));
#6424=CARTESIAN_POINT('Ctrl Pts',(0.938511832204562,0.598550867972523,-0.1524716629431));
#6425=CARTESIAN_POINT('Ctrl Pts',(0.921897120244161,0.57440253785522,-0.130991175878743));
#6426=CARTESIAN_POINT('Ctrl Pts',(0.910735790157152,0.55,-0.112156403618172));
#6427=CARTESIAN_POINT('Origin',(1.1,0.55,0.));
#6428=CARTESIAN_POINT('Origin',(-0.339918693812442,0.,1.04616216792467));
#6429=CARTESIAN_POINT('',(-0.388099915049348,0.55,0.831502973106184));
#6430=CARTESIAN_POINT('',(-0.559918693812442,0.63912556124056,1.04616216792335));
#6431=CARTESIAN_POINT('Ctrl Pts',(-0.388099915049348,0.55,0.831502973106184));
#6432=CARTESIAN_POINT('Ctrl Pts',(-0.400811235892709,0.564520591324655,
0.83435608621082));
#6433=CARTESIAN_POINT('Ctrl Pts',(-0.414489441774859,0.578350901074077,
0.838641228510082));
#6434=CARTESIAN_POINT('Ctrl Pts',(-0.442060797330417,0.603582622702572,
0.85072830691315));
#6435=CARTESIAN_POINT('Ctrl Pts',(-0.456158463572915,0.615143118816555,
0.858605324728243));
#6436=CARTESIAN_POINT('Ctrl Pts',(-0.484752922098353,0.635707573307249,
0.879540531101799));
#6437=CARTESIAN_POINT('Ctrl Pts',(-0.499051049160275,0.644312375876114,
0.892876836196423));
#6438=CARTESIAN_POINT('Ctrl Pts',(-0.523795769282349,0.655446685849627,
0.923864041185001));
#6439=CARTESIAN_POINT('Ctrl Pts',(-0.533985305944486,0.658130838683679,
0.94064383036911));
#6440=CARTESIAN_POINT('Ctrl Pts',(-0.550361643571044,0.657849180985917,
0.978549783037899));
#6441=CARTESIAN_POINT('Ctrl Pts',(-0.555779214799254,0.654458884420129,
0.998971235859072));
#6442=CARTESIAN_POINT('Ctrl Pts',(-0.559392545156816,0.645810916558875,
1.02843094760825));
#6443=CARTESIAN_POINT('Ctrl Pts',(-0.559918693812336,0.642672103940655,
1.03737495240447));
#6444=CARTESIAN_POINT('Ctrl Pts',(-0.559918693812442,0.63912556124056,1.04616216792202));
#6445=CARTESIAN_POINT('',(-0.174765758038764,0.55,0.900819442598166));
#6446=CARTESIAN_POINT('Origin',(-0.339918693812442,0.55,1.04616216792467));
#6447=CARTESIAN_POINT('',(-0.267986765351098,0.55,1.25407031511432));
#6448=CARTESIAN_POINT('Ctrl Pts',(-0.267986765351098,0.55,1.25407031511432));
#6449=CARTESIAN_POINT('Ctrl Pts',(-0.253293148857989,0.564667428121554,
1.24898662703038));
#6450=CARTESIAN_POINT('Ctrl Pts',(-0.238057625599671,0.578482229661416,
1.2419316754898));
#6451=CARTESIAN_POINT('Ctrl Pts',(-0.208963044113738,0.603467206297434,
1.22375112901188));
#6452=CARTESIAN_POINT('Ctrl Pts',(-0.194942594271843,0.614783224033247,
1.21267059279651));
#6453=CARTESIAN_POINT('Ctrl Pts',(-0.16782911650589,0.635319330100662,1.18473227113195));
#6454=CARTESIAN_POINT('Ctrl Pts',(-0.155029153917438,0.644168216758557,
1.16745023332297));
#6455=CARTESIAN_POINT('Ctrl Pts',(-0.135809963569082,0.655254671849834,
1.13051582480638));
#6456=CARTESIAN_POINT('Ctrl Pts',(-0.129007044228756,0.658058624819753,
1.11187531830365));
#6457=CARTESIAN_POINT('Ctrl Pts',(-0.120490750673683,0.657937930401817,
1.07214483106283));
#6458=CARTESIAN_POINT('Ctrl Pts',(-0.119110975535071,0.654856173275339,
1.05193102477361));
#6459=CARTESIAN_POINT('Ctrl Pts',(-0.121836675927961,0.64191056343947,1.00894801471422));
#6460=CARTESIAN_POINT('Ctrl Pts',(-0.126905360909727,0.631232140955598,
0.987436230688157));
#6461=CARTESIAN_POINT('Ctrl Pts',(-0.14498964584378,0.598578363965739,0.939719972286297));
#6462=CARTESIAN_POINT('Ctrl Pts',(-0.160293285605306,0.574417013842144,
0.917264512724103));
#6463=CARTESIAN_POINT('Ctrl Pts',(-0.174765758038764,0.55,0.900819442598166));
#6464=CARTESIAN_POINT('',(-0.52031818912536,0.55,1.17208286555157));
#6465=CARTESIAN_POINT('Origin',(-0.339918693812442,0.55,1.04616216792467));
#6466=CARTESIAN_POINT('Ctrl Pts',(-0.559918693812442,0.63912556124056,1.04616216792202));
#6467=CARTESIAN_POINT('Ctrl Pts',(-0.559918693812632,0.632745440529119,
1.0619700970689));
#6468=CARTESIAN_POINT('Ctrl Pts',(-0.558211019996387,0.625046304728133,
1.07727082028465));
#6469=CARTESIAN_POINT('Ctrl Pts',(-0.548343966268834,0.59726581676475,1.12384601890666));
#6470=CARTESIAN_POINT('Ctrl Pts',(-0.534981138426803,0.574166902399578,
1.15107608347657));
#6471=CARTESIAN_POINT('Ctrl Pts',(-0.52031818912536,0.55,1.17208286555157));
#6472=CARTESIAN_POINT('',(-0.559918693812442,0.9,1.04616216792467));
#6473=CARTESIAN_POINT('',(-0.559918693812442,0.,1.04616216792467));
#6474=CARTESIAN_POINT('Origin',(-0.339918693812442,0.9,1.04616216792467));
#6475=CARTESIAN_POINT('Origin',(0.889918693812442,0.,0.64656377752172));
#6476=CARTESIAN_POINT('',(0.670876851625708,0.55,0.626053502744384));
#6477=CARTESIAN_POINT('',(0.669918693812442,0.571311877390354,0.646563777525436));
#6478=CARTESIAN_POINT('Ctrl Pts',(0.670876851625708,0.55,0.626053502744384));
#6479=CARTESIAN_POINT('Ctrl Pts',(0.670266054477489,0.55730245080333,0.632576581250196));
#6480=CARTESIAN_POINT('Ctrl Pts',(0.669918693812202,0.564427939654626,0.639446501589323));
#6481=CARTESIAN_POINT('Ctrl Pts',(0.669918693812442,0.571311877390354,0.646563777529151));
#6482=CARTESIAN_POINT('',(0.802724611619556,0.55,0.444580629634229));
#6483=CARTESIAN_POINT('Origin',(0.889918693812442,0.55,0.64656377752172));
#6484=CARTESIAN_POINT('',(1.10987928032073,0.55,0.642399598979491));
#6485=CARTESIAN_POINT('Ctrl Pts',(1.10987928032073,0.55,0.642399598979492));
#6486=CARTESIAN_POINT('Ctrl Pts',(1.10958615470441,0.564609024168173,0.626916093209465));
#6487=CARTESIAN_POINT('Ctrl Pts',(1.10759949863652,0.57837155464205,0.610317305256213));
#6488=CARTESIAN_POINT('Ctrl Pts',(1.09937906630242,0.60323879864967,0.577213727602756));
#6489=CARTESIAN_POINT('Ctrl Pts',(1.09324919553707,0.614494006479294,0.560572493545201));
#6490=CARTESIAN_POINT('Ctrl Pts',(1.07518267284658,0.635086936255167,0.526160358808754));
#6491=CARTESIAN_POINT('Ctrl Pts',(1.06268941040781,0.644016986499169,0.508543409408807));
#6492=CARTESIAN_POINT('Ctrl Pts',(1.03345553095711,0.655200788127591,0.478711490622469));
#6493=CARTESIAN_POINT('Ctrl Pts',(1.0178159360962,0.658037254761758,0.466436266197514));
#6494=CARTESIAN_POINT('Ctrl Pts',(0.982652377717061,0.657961095551765,0.446004761419876));
#6495=CARTESIAN_POINT('Ctrl Pts',(0.963865544104577,0.654904186336904,0.438426323310488));
#6496=CARTESIAN_POINT('Ctrl Pts',(0.922132837036694,0.642003792826706,0.427684817450471));
#6497=CARTESIAN_POINT('Ctrl Pts',(0.900086381736093,0.631337654594768,0.425835547406595));
#6498=CARTESIAN_POINT('Ctrl Pts',(0.849024073352859,0.59867163184717,0.428254106385369));
#6499=CARTESIAN_POINT('Ctrl Pts',(0.822877500049851,0.57446613016906,0.435880831514467));
#6500=CARTESIAN_POINT('Ctrl Pts',(0.802724611619556,0.55,0.444580629634229));
#6501=CARTESIAN_POINT('',(0.953929883998579,0.55,0.857045528585688));
#6502=CARTESIAN_POINT('Origin',(0.889918693812442,0.55,0.64656377752172));
#6503=CARTESIAN_POINT('Ctrl Pts',(0.669918693812442,0.571311877390354,0.646563777529151));
#6504=CARTESIAN_POINT('Ctrl Pts',(0.66991869381268,0.57812548596788,0.65360834043107));
#6505=CARTESIAN_POINT('Ctrl Pts',(0.670258663808197,0.58470167519502,0.66089598362366));
#6506=CARTESIAN_POINT('Ctrl Pts',(0.672482969531502,0.603533376354093,0.683258687714869));
#6507=CARTESIAN_POINT('Ctrl Pts',(0.675592903940687,0.615031149045687,0.699004528749127));
#6508=CARTESIAN_POINT('Ctrl Pts',(0.686609461544844,0.635610628918897,0.732627526493686));
#6509=CARTESIAN_POINT('Ctrl Pts',(0.694884092102898,0.644260777278176,0.750408507220998));
#6510=CARTESIAN_POINT('Ctrl Pts',(0.716725112096974,0.655427509796644,0.783571551911549));
#6511=CARTESIAN_POINT('Ctrl Pts',(0.729520363220728,0.65812029334222,0.798445101607854));
#6512=CARTESIAN_POINT('Ctrl Pts',(0.760487823778074,0.657862066752901,0.825743319709735));
#6513=CARTESIAN_POINT('Ctrl Pts',(0.778230186437555,0.654483119781693,0.837216662588005));
#6514=CARTESIAN_POINT('Ctrl Pts',(0.820018109421027,0.641069161130152,0.856722945878246));
#6515=CARTESIAN_POINT('Ctrl Pts',(0.843800606133156,0.629882880868174,0.862908527531438));
#6516=CARTESIAN_POINT('Ctrl Pts',(0.899368376134038,0.597285070273298,0.868796870135415));
#6517=CARTESIAN_POINT('Ctrl Pts',(0.929409465330792,0.574177434161679,0.864502617738802));
#6518=CARTESIAN_POINT('Ctrl Pts',(0.95392988399858,0.55,0.857045528585688));
#6519=CARTESIAN_POINT('',(0.669918693812442,0.9,0.64656377752172));
#6520=CARTESIAN_POINT('',(0.669918693812442,0.,0.64656377752172));
#6521=CARTESIAN_POINT('Origin',(0.889918693812442,0.9,0.64656377752172));
#6522=CARTESIAN_POINT('Origin',(0.339918693812442,0.,1.04616216792467));
#6523=CARTESIAN_POINT('',(0.174765758038764,0.55,0.900819442598166));
#6524=CARTESIAN_POINT('',(0.119918693812442,0.652623283223421,1.04616216792467));
#6525=CARTESIAN_POINT('Ctrl Pts',(0.174765758038763,0.55,0.900819442598166));
#6526=CARTESIAN_POINT('Ctrl Pts',(0.16615910126156,0.564520591324654,0.910599186515576));
#6527=CARTESIAN_POINT('Ctrl Pts',(0.157611943697822,0.578350901074076,0.922105787154341));
#6528=CARTESIAN_POINT('Ctrl Pts',(0.142410854924047,0.603582622702572,0.948090475176036));
#6529=CARTESIAN_POINT('Ctrl Pts',(0.135635598256597,0.615143118816555,0.962749516762522));
#6530=CARTESIAN_POINT('Ctrl Pts',(0.124807600924644,0.635707573307249,0.996493855518017));
#6531=CARTESIAN_POINT('Ctrl Pts',(0.12107905659851,0.644312375876114,1.01568738120414));
#6532=CARTESIAN_POINT('Ctrl Pts',(0.119995150322276,0.65099826710225,1.03947451044843));
#6533=CARTESIAN_POINT('Ctrl Pts',(0.119918693812442,0.651851819062756,1.04281359823645));
#6534=CARTESIAN_POINT('Ctrl Pts',(0.119918693812442,0.652623283223421,1.04616216792467));
#6535=CARTESIAN_POINT('',(0.388099915049348,0.55,0.831502973106184));
#6536=CARTESIAN_POINT('Origin',(0.339918693812442,0.55,1.04616216792467));
#6537=CARTESIAN_POINT('',(0.52031818912536,0.55,1.17208286555157));
#6538=CARTESIAN_POINT('Ctrl Pts',(0.52031818912536,0.55,1.17208286555157));
#6539=CARTESIAN_POINT('Ctrl Pts',(0.529217457694123,0.564667428121555,1.15933338442007));
#6540=CARTESIAN_POINT('Ctrl Pts',(0.537396458457103,0.578482229661417,1.14467059284705));
#6541=CARTESIAN_POINT('Ctrl Pts',(0.550248212225113,0.603467206297435,1.11286085586034));
#6542=CARTESIAN_POINT('Ctrl Pts',(0.555078018641098,0.614783224033248,1.09565550010774));
#6543=CARTESIAN_POINT('Ctrl Pts',(0.560591549482129,0.635319330100661,1.05711602071761));
#6544=CARTESIAN_POINT('Ctrl Pts',(0.56078880978987,0.644168216758556,1.03561092919333));
#6545=CARTESIAN_POINT('Ctrl Pts',(0.554627960771623,0.655254671849834,0.994433608378459));
#6546=CARTESIAN_POINT('Ctrl Pts',(0.549175023311743,0.658058624819753,0.975354466173215));
#6547=CARTESIAN_POINT('Ctrl Pts',(0.532711855060331,0.657937930401817,0.938206075044727));
#6548=CARTESIAN_POINT('Ctrl Pts',(0.521946739366385,0.654856173275339,0.921041750757787));
#6549=CARTESIAN_POINT('Ctrl Pts',(0.494476822014916,0.64191056343947,0.887869891643463));
#6550=CARTESIAN_POINT('Ctrl Pts',(0.477731860324512,0.631232140955599,0.873445791067851));
#6551=CARTESIAN_POINT('Ctrl Pts',(0.435054453498551,0.598578363965736,0.84547220309525));
#6552=CARTESIAN_POINT('Ctrl Pts',(0.409474560891576,0.57441701384214,0.836300608451158));
#6553=CARTESIAN_POINT('Ctrl Pts',(0.388099915049349,0.55,0.831502973106184));
#6554=CARTESIAN_POINT('',(0.267986765351098,0.55,1.25407031511432));
#6555=CARTESIAN_POINT('Origin',(0.339918693812442,0.55,1.04616216792467));
#6556=CARTESIAN_POINT('Ctrl Pts',(0.119918693812442,0.652623283223421,1.04616216792467));
#6557=CARTESIAN_POINT('Ctrl Pts',(0.119918693812442,0.656293518143051,1.0620929629339));
#6558=CARTESIAN_POINT('Ctrl Pts',(0.121649354618456,0.658107263715709,1.07823803146977));
#6559=CARTESIAN_POINT('Ctrl Pts',(0.129925208402575,0.657849180985917,1.11515786183808));
#6560=CARTESIAN_POINT('Ctrl Pts',(0.137545730009388,0.654458884420129,1.13486353269143));
#6561=CARTESIAN_POINT('Ctrl Pts',(0.15989407549514,0.64103073977944,1.17516872094799));
#6562=CARTESIAN_POINT('Ctrl Pts',(0.175488151194729,0.629849556228346,1.19412647612185));
#6563=CARTESIAN_POINT('Ctrl Pts',(0.21696052828649,0.597265816764751,1.23151902491249));
#6564=CARTESIAN_POINT('Ctrl Pts',(0.24377671347677,0.574166902399579,1.24569413677302));
#6565=CARTESIAN_POINT('Ctrl Pts',(0.267986765351098,0.55,1.25407031511432));
#6566=CARTESIAN_POINT('',(0.119918693812442,0.9,1.04616216792467));
#6567=CARTESIAN_POINT('',(0.119918693812442,0.,1.04616216792467));
#6568=CARTESIAN_POINT('Origin',(0.339918693812442,0.9,1.04616216792467));
#6569=CARTESIAN_POINT('Origin',(-0.889918693812442,0.,0.646563777521721));
#6570=CARTESIAN_POINT('',(-0.802724611619556,0.55,0.444580629634229));
#6571=CARTESIAN_POINT('',(-1.10987928032073,0.55,0.642399598979491));
#6572=CARTESIAN_POINT('Ctrl Pts',(-0.802724611619556,0.55,0.444580629634229));
#6573=CARTESIAN_POINT('Ctrl Pts',(-0.814693298418458,0.564530296745673,
0.439413868588077));
#6574=CARTESIAN_POINT('Ctrl Pts',(-0.828288194978147,0.578369513099121,
0.434838103866291));
#6575=CARTESIAN_POINT('Ctrl Pts',(-0.857626293279466,0.603533376354093,
0.428430764212231));
#6576=CARTESIAN_POINT('Ctrl Pts',(-0.873562500583475,0.615031149045687,
0.426522755127025));
#6577=CARTESIAN_POINT('Ctrl Pts',(-0.908944175205009,0.635610628918897,
0.426610046318699));
#6578=CARTESIAN_POINT('Ctrl Pts',(-0.928411894256451,0.644260777278176,
0.428985062409479));
#6579=CARTESIAN_POINT('Ctrl Pts',(-0.96670107036224,0.655427509796644,0.439509162402782));
#6580=CARTESIAN_POINT('Ctrl Pts',(-0.984800606765885,0.65812029334222,0.447081989738822));
#6581=CARTESIAN_POINT('Ctrl Pts',(-1.02033222655978,0.657862066752901,0.468098181585364));
#6582=CARTESIAN_POINT('Ctrl Pts',(-1.03672671564999,0.654483119781693,0.48142671327546));
#6583=CARTESIAN_POINT('Ctrl Pts',(-1.0681914718434,0.641069161130152,0.515141616697554));
#6584=CARTESIAN_POINT('Ctrl Pts',(-1.08142350523446,0.629882880868174,0.535848665318463));
#6585=CARTESIAN_POINT('Ctrl Pts',(-1.10419503710793,0.597285070273303,0.586877157140452));
#6586=CARTESIAN_POINT('Ctrl Pts',(-1.10939416747485,0.574177434161687,0.616774927746317));
#6587=CARTESIAN_POINT('Ctrl Pts',(-1.10987928032073,0.55,0.642399598979492));
#6588=CARTESIAN_POINT('',(-0.670876851625708,0.55,0.626053502744384));
#6589=CARTESIAN_POINT('Origin',(-0.889918693812442,0.55,0.646563777521721));
#6590=CARTESIAN_POINT('',(-0.953929883998579,0.55,0.857045528585689));
#6591=CARTESIAN_POINT('Ctrl Pts',(-0.95392988399858,0.55,0.857045528585688));
#6592=CARTESIAN_POINT('Ctrl Pts',(-0.939113614143975,0.564609024168171,
0.861551415973636));
#6593=CARTESIAN_POINT('Ctrl Pts',(-0.922713318211477,0.57837155464205,0.864791301338213));
#6594=CARTESIAN_POINT('Ctrl Pts',(-0.888689691679124,0.603238798649673,
0.867202773669637));
#6595=CARTESIAN_POINT('Ctrl Pts',(-0.870968703349679,0.614494006479295,
0.866515344265355));
#6596=CARTESIAN_POINT('Ctrl Pts',(-0.832657955828337,0.635086936255166,
0.859966994580058));
#6597=CARTESIAN_POINT('Ctrl Pts',(-0.812042610895507,0.644016986499169,
0.853529132681505));
#6598=CARTESIAN_POINT('Ctrl Pts',(-0.774637004578397,0.655200788127591,
0.834944631013122));
#6599=CARTESIAN_POINT('Ctrl Pts',(-0.758129671802899,0.658037254761758,
0.823863745365518));
#6600=CARTESIAN_POINT('Ctrl Pts',(-0.727832018924561,0.657961095551765,
0.796734896229852));
#6601=CARTESIAN_POINT('Ctrl Pts',(-0.714819045120535,0.654904186336905,
0.781209421868766));
#6602=CARTESIAN_POINT('Ctrl Pts',(-0.691707150272296,0.642003792826706,
0.744838566725142));
#6603=CARTESIAN_POINT('Ctrl Pts',(-0.683135660593065,0.631337654594768,
0.724442597621041));
#6604=CARTESIAN_POINT('Ctrl Pts',(-0.669656725807439,0.598671631847171,
0.675132080669756));
#6605=CARTESIAN_POINT('Ctrl Pts',(-0.668830436944159,0.574466130169061,
0.647908424074824));
#6606=CARTESIAN_POINT('Ctrl Pts',(-0.670876851625708,0.55,0.626053502744384));
#6607=CARTESIAN_POINT('',(-1.10991869381244,0.55,0.646563777521721));
#6608=CARTESIAN_POINT('Origin',(-0.889918693812442,0.55,0.646563777521721));
#6609=CARTESIAN_POINT('',(-1.10991869381244,0.9,0.646563777521721));
#6610=CARTESIAN_POINT('',(-1.10991869381244,0.,0.646563777521721));
#6611=CARTESIAN_POINT('Origin',(-0.889918693812442,0.9,0.646563777521721));
#6612=CARTESIAN_POINT('Origin',(-0.889918693812442,0.55,0.646563777521721));
#6613=CARTESIAN_POINT('Origin',(-1.1,0.,1.34711147906209E-16));
#6614=CARTESIAN_POINT('',(-0.910735790157152,0.55,-0.112156403618172));
#6615=CARTESIAN_POINT('',(-1.27550420984285,0.55,-0.132658480043447));
#6616=CARTESIAN_POINT('Ctrl Pts',(-0.910735790157152,0.55,-0.112156403618172));
#6617=CARTESIAN_POINT('Ctrl Pts',(-0.917376089752458,0.564517997495035,
-0.123361925688084));
#6618=CARTESIAN_POINT('Ctrl Pts',(-0.925676503375737,0.578345926844046,
-0.135044303040797));
#6619=CARTESIAN_POINT('Ctrl Pts',(-0.945705763566753,0.603597412340976,
-0.157548233557299));
#6620=CARTESIAN_POINT('Ctrl Pts',(-0.957575956315956,0.615176011910307,
-0.168539952403237));
#6621=CARTESIAN_POINT('Ctrl Pts',(-0.986343324120607,0.635735932391,-0.189265250815529));
#6622=CARTESIAN_POINT('Ctrl Pts',(-1.00343254919411,0.644327528980788,-0.198729556237649));
#6623=CARTESIAN_POINT('Ctrl Pts',(-1.04053658704398,0.65545235887726,-0.212677811623889));
#6624=CARTESIAN_POINT('Ctrl Pts',(-1.05964780090184,0.658133955563747,-0.217181471497843));
#6625=CARTESIAN_POINT('Ctrl Pts',(-1.1007627783985,0.657845346648502,-0.221036398352684));
#6626=CARTESIAN_POINT('Ctrl Pts',(-1.12185832284616,0.65445169739566,-0.219874810080966));
#6627=CARTESIAN_POINT('Ctrl Pts',(-1.16708666484378,0.641019397008994,-0.211069922924208));
#6628=CARTESIAN_POINT('Ctrl Pts',(-1.18992721371268,0.629839760817717,-0.202098025620397));
#6629=CARTESIAN_POINT('Ctrl Pts',(-1.23829403807688,0.597260212402138,-0.174213524003119));
#6630=CARTESIAN_POINT('Ctrl Pts',(-1.2600586328202,0.57416383696199,-0.153092633895047));
#6631=CARTESIAN_POINT('Ctrl Pts',(-1.27550420984285,0.55,-0.132658480043447));
#6632=CARTESIAN_POINT('',(-0.910735790157152,0.55,0.112156403618172));
#6633=CARTESIAN_POINT('Origin',(-1.1,0.55,1.34711147906209E-16));
#6634=CARTESIAN_POINT('',(-1.27550420984285,0.55,0.132658480043447));
#6635=CARTESIAN_POINT('Ctrl Pts',(-1.27550420984285,0.55,0.132658480043447));
#6636=CARTESIAN_POINT('Ctrl Pts',(-1.26611782177473,0.56468453723726,0.145076462072449));
#6637=CARTESIAN_POINT('Ctrl Pts',(-1.25468431627751,0.578514647841062,0.157400492027332));
#6638=CARTESIAN_POINT('Ctrl Pts',(-1.22835219222699,0.603533958896827,0.179483010322184));
#6639=CARTESIAN_POINT('Ctrl Pts',(-1.21344338101808,0.614867643252025,0.189407731207314));
#6640=CARTESIAN_POINT('Ctrl Pts',(-1.17846267135551,0.635387178695069,0.206540975098488));
#6641=CARTESIAN_POINT('Ctrl Pts',(-1.15809147022147,0.644212495667266,0.213351934557227));
#6642=CARTESIAN_POINT('Ctrl Pts',(-1.11706033563968,0.65527050791581,0.220191916744403));
#6643=CARTESIAN_POINT('Ctrl Pts',(-1.09724086630217,0.658064897233583,0.220893276198431));
#6644=CARTESIAN_POINT('Ctrl Pts',(-1.05683477389847,0.657931008613642,0.216703862540943));
#6645=CARTESIAN_POINT('Ctrl Pts',(-1.03718465931368,0.654841874466928,0.211762979306541));
#6646=CARTESIAN_POINT('Ctrl Pts',(-0.997159417898573,0.641882889790503,
0.195877882014933));
#6647=CARTESIAN_POINT('Ctrl Pts',(-0.978275892037171,0.631200912596757,
0.184408191234794));
#6648=CARTESIAN_POINT('Ctrl Pts',(-0.938511832204561,0.598550867972523,
0.1524716629431));
#6649=CARTESIAN_POINT('Ctrl Pts',(-0.921897120244161,0.57440253785522,0.130991175878743));
#6650=CARTESIAN_POINT('Ctrl Pts',(-0.910735790157152,0.55,0.112156403618173));
#6651=CARTESIAN_POINT('',(-1.32,0.55,1.61653377487451E-16));
#6652=CARTESIAN_POINT('Origin',(-1.1,0.55,1.34711147906209E-16));
#6653=CARTESIAN_POINT('',(-1.32,0.9,1.61653377487451E-16));
#6654=CARTESIAN_POINT('',(-1.32,0.,1.61653377487451E-16));
#6655=CARTESIAN_POINT('Origin',(-1.1,0.9,1.34711147906209E-16));
#6656=CARTESIAN_POINT('Origin',(-1.1,0.55,1.34711147906209E-16));
#6657=CARTESIAN_POINT('Origin',(-0.339918693812442,0.,-1.04616216792467));
#6658=CARTESIAN_POINT('',(-0.174765758038764,0.55,-0.900819442598166));
#6659=CARTESIAN_POINT('',(-0.267986765351098,0.55,-1.25407031511432));
#6660=CARTESIAN_POINT('Ctrl Pts',(-0.174765758038764,0.55,-0.900819442598166));
#6661=CARTESIAN_POINT('Ctrl Pts',(-0.16615910126156,0.564520591324654,-0.910599186515576));
#6662=CARTESIAN_POINT('Ctrl Pts',(-0.157611943697822,0.578350901074076,
-0.922105787154341));
#6663=CARTESIAN_POINT('Ctrl Pts',(-0.142410854924047,0.603582622702572,
-0.948090475176037));
#6664=CARTESIAN_POINT('Ctrl Pts',(-0.135635598256598,0.615143118816555,
-0.962749516762522));
#6665=CARTESIAN_POINT('Ctrl Pts',(-0.124807600924644,0.635707573307249,
-0.996493855518017));
#6666=CARTESIAN_POINT('Ctrl Pts',(-0.12107905659851,0.644312375876114,-1.01568738120414));
#6667=CARTESIAN_POINT('Ctrl Pts',(-0.11927397960075,0.655446685849627,-1.05530113820794));
#6668=CARTESIAN_POINT('Ctrl Pts',(-0.120893383895271,0.658130838683679,
-1.07486553219761));
#6669=CARTESIAN_POINT('Ctrl Pts',(-0.129925208402575,0.657849180985917,
-1.11515786183808));
#6670=CARTESIAN_POINT('Ctrl Pts',(-0.137545730009389,0.654458884420129,
-1.13486353269143));
#6671=CARTESIAN_POINT('Ctrl Pts',(-0.15989407549514,0.64103073977944,-1.17516872094799));
#6672=CARTESIAN_POINT('Ctrl Pts',(-0.175488151194729,0.629849556228346,
-1.19412647612185));
#6673=CARTESIAN_POINT('Ctrl Pts',(-0.216960528286492,0.59726581676475,-1.2315190249125));
#6674=CARTESIAN_POINT('Ctrl Pts',(-0.243776713476771,0.574166902399578,
-1.24569413677302));
#6675=CARTESIAN_POINT('Ctrl Pts',(-0.267986765351099,0.55,-1.25407031511432));
#6676=CARTESIAN_POINT('',(-0.388099915049348,0.55,-0.831502973106184));
#6677=CARTESIAN_POINT('Origin',(-0.339918693812442,0.55,-1.04616216792467));
#6678=CARTESIAN_POINT('',(-0.559918693812442,0.639125561239885,-1.04616216792418));
#6679=CARTESIAN_POINT('Ctrl Pts',(-0.559918693812442,0.639125561239885,
-1.04616216792369));
#6680=CARTESIAN_POINT('Ctrl Pts',(-0.559918693812395,0.643427932070251,
-1.03550224841357));
#6681=CARTESIAN_POINT('Ctrl Pts',(-0.55914412823418,0.647127823162253,-1.02461835660206));
#6682=CARTESIAN_POINT('Ctrl Pts',(-0.554627960771623,0.655254671849834,
-0.994433608378459));
#6683=CARTESIAN_POINT('Ctrl Pts',(-0.549175023311743,0.658058624819753,
-0.975354466173216));
#6684=CARTESIAN_POINT('Ctrl Pts',(-0.532711855060331,0.657937930401817,
-0.938206075044727));
#6685=CARTESIAN_POINT('Ctrl Pts',(-0.521946739366384,0.654856173275339,
-0.921041750757787));
#6686=CARTESIAN_POINT('Ctrl Pts',(-0.494476822014917,0.64191056343947,-0.887869891643464));
#6687=CARTESIAN_POINT('Ctrl Pts',(-0.477731860324512,0.631232140955599,
-0.873445791067852));
#6688=CARTESIAN_POINT('Ctrl Pts',(-0.435054453498552,0.598578363965737,
-0.84547220309525));
#6689=CARTESIAN_POINT('Ctrl Pts',(-0.409474560891577,0.574417013842142,
-0.836300608451158));
#6690=CARTESIAN_POINT('Ctrl Pts',(-0.388099915049349,0.55,-0.831502973106184));
#6691=CARTESIAN_POINT('',(-0.559918693812442,0.9,-1.04616216792467));
#6692=CARTESIAN_POINT('',(-0.559918693812442,0.,-1.04616216792467));
#6693=CARTESIAN_POINT('Origin',(-0.339918693812442,0.9,-1.04616216792467));
#6694=CARTESIAN_POINT('',(-0.52031818912536,0.55,-1.17208286555157));
#6695=CARTESIAN_POINT('Ctrl Pts',(-0.52031818912536,0.55,-1.17208286555157));
#6696=CARTESIAN_POINT('Ctrl Pts',(-0.529217457694122,0.564667428121554,
-1.15933338442007));
#6697=CARTESIAN_POINT('Ctrl Pts',(-0.537396458457103,0.578482229661416,
-1.14467059284705));
#6698=CARTESIAN_POINT('Ctrl Pts',(-0.550248212225112,0.603467206297434,
-1.11286085586034));
#6699=CARTESIAN_POINT('Ctrl Pts',(-0.555078018641099,0.614783224033247,
-1.09565550010774));
#6700=CARTESIAN_POINT('Ctrl Pts',(-0.559145317472554,0.629932587049239,
-1.06722515592215));
#6701=CARTESIAN_POINT('Ctrl Pts',(-0.559918693812489,0.634829883465696,
-1.05680550414918));
#6702=CARTESIAN_POINT('Ctrl Pts',(-0.559918693812442,0.639125561239885,
-1.04616216792369));
#6703=CARTESIAN_POINT('Origin',(-0.339918693812442,0.55,-1.04616216792467));
#6704=CARTESIAN_POINT('Origin',(0.889918693812442,0.,-0.646563777521721));
#6705=CARTESIAN_POINT('',(0.802724611619556,0.55,-0.444580629634229));
#6706=CARTESIAN_POINT('',(1.10987928032073,0.55,-0.642399598979491));
#6707=CARTESIAN_POINT('Ctrl Pts',(0.802724611619556,0.55,-0.444580629634229));
#6708=CARTESIAN_POINT('Ctrl Pts',(0.814693298418457,0.564530296745673,-0.439413868588077));
#6709=CARTESIAN_POINT('Ctrl Pts',(0.828288194978146,0.578369513099121,-0.434838103866291));
#6710=CARTESIAN_POINT('Ctrl Pts',(0.857626293279466,0.603533376354093,-0.428430764212231));
#6711=CARTESIAN_POINT('Ctrl Pts',(0.873562500583474,0.615031149045687,-0.426522755127025));
#6712=CARTESIAN_POINT('Ctrl Pts',(0.908944175205009,0.635610628918897,-0.426610046318699));
#6713=CARTESIAN_POINT('Ctrl Pts',(0.928411894256451,0.644260777278176,-0.428985062409479));
#6714=CARTESIAN_POINT('Ctrl Pts',(0.96670107036224,0.655427509796644,-0.439509162402782));
#6715=CARTESIAN_POINT('Ctrl Pts',(0.984800606765885,0.65812029334222,-0.447081989738822));
#6716=CARTESIAN_POINT('Ctrl Pts',(1.02033222655978,0.657862066752901,-0.468098181585364));
#6717=CARTESIAN_POINT('Ctrl Pts',(1.03672671564999,0.654483119781693,-0.481426713275459));
#6718=CARTESIAN_POINT('Ctrl Pts',(1.0681914718434,0.641069161130152,-0.515141616697554));
#6719=CARTESIAN_POINT('Ctrl Pts',(1.08142350523446,0.629882880868174,-0.535848665318462));
#6720=CARTESIAN_POINT('Ctrl Pts',(1.10419503710794,0.597285070273298,-0.58687715714046));
#6721=CARTESIAN_POINT('Ctrl Pts',(1.10939416747485,0.574177434161679,-0.616774927746326));
#6722=CARTESIAN_POINT('Ctrl Pts',(1.10987928032073,0.55,-0.642399598979492));
#6723=CARTESIAN_POINT('',(0.670876851625708,0.55,-0.626053502744384));
#6724=CARTESIAN_POINT('Origin',(0.889918693812442,0.55,-0.646563777521721));
#6725=CARTESIAN_POINT('',(0.669918693812442,0.571311877460243,-0.646563777561565));
#6726=CARTESIAN_POINT('Ctrl Pts',(0.669918693812442,0.571311877460243,-0.646563777601409));
#6727=CARTESIAN_POINT('Ctrl Pts',(0.669918693809818,0.564304796586028,-0.639319184455347));
#6728=CARTESIAN_POINT('Ctrl Pts',(0.670277510265801,0.557165489897726,-0.632454237839258));
#6729=CARTESIAN_POINT('Ctrl Pts',(0.670876851625708,0.55,-0.626053502744384));
#6730=CARTESIAN_POINT('',(0.669918693812442,0.9,-0.646563777521721));
#6731=CARTESIAN_POINT('',(0.669918693812442,0.,-0.646563777521721));
#6732=CARTESIAN_POINT('Origin',(0.889918693812442,0.9,-0.646563777521721));
#6733=CARTESIAN_POINT('',(0.953929883998579,0.55,-0.857045528585689));
#6734=CARTESIAN_POINT('Ctrl Pts',(0.953929883998579,0.55,-0.857045528585689));
#6735=CARTESIAN_POINT('Ctrl Pts',(0.939113614143974,0.564609024168172,-0.861551415973636));
#6736=CARTESIAN_POINT('Ctrl Pts',(0.922713318211476,0.57837155464205,-0.864791301338213));
#6737=CARTESIAN_POINT('Ctrl Pts',(0.888689691679126,0.603238798649671,-0.867202773669637));
#6738=CARTESIAN_POINT('Ctrl Pts',(0.87096870334968,0.614494006479294,-0.866515344265356));
#6739=CARTESIAN_POINT('Ctrl Pts',(0.832657955828336,0.635086936255167,-0.859966994580058));
#6740=CARTESIAN_POINT('Ctrl Pts',(0.812042610895507,0.644016986499169,-0.853529132681505));
#6741=CARTESIAN_POINT('Ctrl Pts',(0.774637004578397,0.655200788127591,-0.834944631013121));
#6742=CARTESIAN_POINT('Ctrl Pts',(0.758129671802899,0.658037254761758,-0.823863745365518));
#6743=CARTESIAN_POINT('Ctrl Pts',(0.727832018924561,0.657961095551765,-0.796734896229852));
#6744=CARTESIAN_POINT('Ctrl Pts',(0.714819045120535,0.654904186336905,-0.781209421868767));
#6745=CARTESIAN_POINT('Ctrl Pts',(0.691707150272296,0.642003792826706,-0.744838566725142));
#6746=CARTESIAN_POINT('Ctrl Pts',(0.683135660593065,0.631337654594767,-0.72444259762104));
#6747=CARTESIAN_POINT('Ctrl Pts',(0.672013600394922,0.604383486686772,-0.683754327616307));
#6748=CARTESIAN_POINT('Ctrl Pts',(0.669918693818778,0.588230048762875,-0.664055407862729));
#6749=CARTESIAN_POINT('Ctrl Pts',(0.669918693812442,0.571311877460243,-0.646563777601409));
#6750=CARTESIAN_POINT('Origin',(0.889918693812442,0.55,-0.646563777521721));
#6751=CARTESIAN_POINT('Origin',(0.8,0.55,0.));
#6752=CARTESIAN_POINT('Origin',(0.,0.55,0.));
#6753=CARTESIAN_POINT('Origin',(0.,0.55,0.));
#6754=CARTESIAN_POINT('Origin',(0.,0.55,0.));
#6755=CARTESIAN_POINT('Origin',(0.,0.55,0.));
#6756=CARTESIAN_POINT('Origin',(0.,0.55,0.));
#6757=CARTESIAN_POINT('Origin',(0.,0.55,0.));
#6758=CARTESIAN_POINT('Origin',(0.,0.55,0.));
#6759=CARTESIAN_POINT('Origin',(0.,0.55,0.));
#6760=CARTESIAN_POINT('Origin',(0.,0.55,0.));
#6761=CARTESIAN_POINT('Origin',(0.,0.55,0.));
#6762=CARTESIAN_POINT('',(-0.8,0.55,-9.79717439317883E-17));
#6763=CARTESIAN_POINT('Origin',(0.,0.55,0.));
#6764=CARTESIAN_POINT('Origin',(0.,0.45,0.));
#6765=CARTESIAN_POINT('Origin',(0.,0.55,0.));
#6766=CARTESIAN_POINT('Origin',(0.,0.45,0.));
#6767=CARTESIAN_POINT('Origin',(0.,0.55,0.));
#6768=CARTESIAN_POINT('Origin',(0.,0.45,0.));
#6769=CARTESIAN_POINT('Origin',(0.,0.55,0.));
#6770=CARTESIAN_POINT('Origin',(0.,0.45,0.));
#6771=CARTESIAN_POINT('Origin',(0.,0.55,0.));
#6772=CARTESIAN_POINT('Origin',(0.,0.45,0.));
#6773=CARTESIAN_POINT('Origin',(0.,0.55,0.));
#6774=CARTESIAN_POINT('Origin',(0.,0.45,0.));
#6775=CARTESIAN_POINT('Origin',(0.,0.55,0.));
#6776=CARTESIAN_POINT('Origin',(0.,0.45,0.));
#6777=CARTESIAN_POINT('Origin',(0.,0.55,0.));
#6778=CARTESIAN_POINT('Origin',(0.,0.45,0.));
#6779=CARTESIAN_POINT('Origin',(0.,0.55,0.));
#6780=CARTESIAN_POINT('Origin',(0.,0.45,0.));
#6781=CARTESIAN_POINT('Origin',(0.,0.55,0.));
#6782=CARTESIAN_POINT('Origin',(0.,0.45,0.));
#6783=CARTESIAN_POINT('Origin',(0.,0.55,0.));
#6784=CARTESIAN_POINT('Origin',(1.4,0.9,0.));
#6785=CARTESIAN_POINT('',(-1.4,0.9,-1.71450551880629E-16));
#6786=CARTESIAN_POINT('Origin',(0.,0.9,0.));
#6787=CARTESIAN_POINT('',(-0.8,0.9,-9.79717439317883E-17));
#6788=CARTESIAN_POINT('Origin',(0.,0.9,0.));
#6789=CARTESIAN_POINT('Origin',(0.,0.725,0.));
#6790=CARTESIAN_POINT('',(-1.4,0.55,-1.71450551880629E-16));
#6791=CARTESIAN_POINT('Origin',(0.,0.55,0.));
#6792=CARTESIAN_POINT('',(-1.4,0.725,-1.71450551880629E-16));
#6793=CARTESIAN_POINT('Origin',(0.8,0.55,0.));
#6794=CARTESIAN_POINT('Origin',(0.,0.725,0.));
#6795=CARTESIAN_POINT('',(-0.8,0.725,-9.79717439317883E-17));
#7769=UNCERTAINTY_MEASURE_WITH_UNIT(LENGTH_MEASURE(0.001),#7817,
'DISTANCE_ACCURACY_VALUE',
'Maximum model space distance between geometric entities at asserted c
onnectivities');
#7789=UNCERTAINTY_MEASURE_WITH_UNIT(LENGTH_MEASURE(0.001),#7817,
'DISTANCE_ACCURACY_VALUE',
'Maximum model space distance between geometric entities at asserted c
onnectivities');
#7796=(
GEOMETRIC_REPRESENTATION_CONTEXT(3)
GLOBAL_UNCERTAINTY_ASSIGNED_CONTEXT((#7769))
GLOBAL_UNIT_ASSIGNED_CONTEXT((#7817,#7819,#7820))
REPRESENTATION_CONTEXT('','3D')
);
#7816=(
GEOMETRIC_REPRESENTATION_CONTEXT(3)
GLOBAL_UNCERTAINTY_ASSIGNED_CONTEXT((#7789))
GLOBAL_UNIT_ASSIGNED_CONTEXT((#7817,#7819,#7820))
REPRESENTATION_CONTEXT('','3D')
);
#7817=(
LENGTH_UNIT()
NAMED_UNIT(*)
SI_UNIT(.CENTI.,.METRE.)
);
#7819=(
NAMED_UNIT(*)
PLANE_ANGLE_UNIT()
SI_UNIT($,.RADIAN.)
);
#7820=(
NAMED_UNIT(*)
SI_UNIT($,.STERADIAN.)
SOLID_ANGLE_UNIT()
);
#7827=SHAPE_DEFINITION_REPRESENTATION(#7853,#7907);
#7853=PRODUCT_DEFINITION_SHAPE('',$,#7934);
#7907=SHAPE_REPRESENTATION('',(#4089),#7796);
#7927=PRODUCT_DEFINITION_CONTEXT('part definition',#8007,'design');
#7934=PRODUCT_DEFINITION('Housing washer','Housing washer',#7960,#7927);
#7960=PRODUCT_DEFINITION_FORMATION('',$,#8015);
#8007=APPLICATION_CONTEXT(
'Core Data for Automotive Mechanical Design Process');
#8008=PRODUCT_CONTEXT('part definition',#8007,'mechanical');
#8015=PRODUCT('Housing washer','Housing washer','Housing washer',(#8008));
#8098=COLOUR_RGB('Black',0.12,0.14,0.17);
#8099=FILL_AREA_STYLE_COLOUR('',#8098);
#8100=FILL_AREA_STYLE('',(#8099));
#8101=SURFACE_STYLE_FILL_AREA(#8100);
#8102=SURFACE_SIDE_STYLE('',(#8101));
#8103=SURFACE_STYLE_USAGE(.BOTH.,#8102);
#8104=PRESENTATION_STYLE_ASSIGNMENT((#8103));
ENDSEC;
END-ISO-10303-21;
